ISO-10303-21;
HEADER;
FILE_DESCRIPTION (('STEP AP214'),
    '1' );
FILE_NAME ('hex flange nut gradea_iso_ISO - 4161 - M5 - N.step',
    '2026-10-02T06:35:35',
    ( '' ),
    ( '' ),
    'SwSTEP 2.0',
    'SolidWorks 2026',
    '' );
FILE_SCHEMA (( 'AUTOMOTIVE_DESIGN' ));
ENDSEC;

DATA;
#15=AXIS2_PLACEMENT_3D ( 'NONE', #1974, #14669, #772 ) ;
#21=CARTESIAN_POINT ( 'NONE',  ( -3.999999999999996447, 0.000000000000000000, 0.000000000000000000 ) ) ;
#26=ADVANCED_FACE ( 'NONE', ( #7589 ), #2370, .T. ) ;
#64=CARTESIAN_POINT ( 'NONE',  ( 0.000000000000000000, 4.618802153517009401, -0.5000000000000004441 ) ) ;
#71=CARTESIAN_POINT ( 'NONE',  ( 0.000000000000000000, 4.618802153517009401, -3.433295621305381573 ) ) ;
#75=ORIENTED_EDGE ( 'NONE', *, *, #14051, .F. ) ;
#76=FILL_AREA_STYLE ('',( #3580 ) ) ;
#87=CARTESIAN_POINT ( 'NONE',  ( -3.999999999999999112, 2.471528634177587946, -3.686887442155188932 ) ) ;
#93=CARTESIAN_POINT ( 'NONE',  ( -2.344047193898592063, -3.265465875126478679, -8.534280460060699911E-15 ) ) ;
#101=AXIS2_PLACEMENT_3D ( 'NONE', #2141, #150, #5905 ) ;
#104=DIRECTION ( 'NONE',  ( 1.000000000000000000, 0.000000000000000000, 0.000000000000000000 ) ) ;
#123=CARTESIAN_POINT ( 'NONE',  ( 2.836893136758667833, 3.208949435746013545, -3.505054077164964976 ) ) ;
#128=ORIENTED_EDGE ( 'NONE', *, *, #10022, .F. ) ;
#134=CARTESIAN_POINT ( 'NONE',  ( 4.154306624730861763, 2.398490048084776394, -3.721999068284301604 ) ) ;
#150=DIRECTION ( 'NONE',  ( -0.000000000000000000, -0.000000000000000000, 1.000000000000000000 ) ) ;
#157=( NAMED_UNIT ( * ) SI_UNIT ( $, .STERADIAN. ) SOLID_ANGLE_UNIT ( ) );
#183=ORIENTED_EDGE ( 'NONE', *, *, #10022, .T. ) ;
#194=SURFACE_SIDE_STYLE ('',( #3699 ) ) ;
#227=CARTESIAN_POINT ( 'NONE',  ( 3.999999999999996447, -2.309401076758518911, -3.433295621305385126 ) ) ;
#243=B_SPLINE_CURVE_WITH_KNOTS ( 'NONE', 3,
 ( #4332, #3259, #11468, #1065, #15025, #13745 ),
 .UNSPECIFIED., .F., .F.,
 ( 4, 2, 4 ),
 ( -3.640115492410820263E-06, 0.0002066546034003392330, 0.0004169493222930892523 ),
 .UNSPECIFIED. ) ;
#278=( LENGTH_UNIT ( ) NAMED_UNIT ( * ) SI_UNIT ( .MILLI., .METRE. ) );
#294=VECTOR ( 'NONE', #9965, 1000.000000000000000 ) ;
#296=CARTESIAN_POINT ( 'NONE',  ( 0.000000000000000000, 0.000000000000000000, 0.000000000000000000 ) ) ;
#306=CARTESIAN_POINT ( 'NONE',  ( 2.166671187435639459E-31, -4.618802153517023612, -3.504271511727135024 ) ) ;
#309=AXIS2_PLACEMENT_3D ( 'NONE', #3603, #2453, #104 ) ;
#319=ORIENTED_EDGE ( 'NONE', *, *, #3102, .F. ) ;
#349=CARTESIAN_POINT ( 'NONE',  ( 0.000000000000000000, 0.000000000000000000, -4.000000000000000000 ) ) ;
#362=VERTEX_POINT ( 'NONE', #7552 ) ;
#372=CARTESIAN_POINT ( 'NONE',  ( -4.101948962586058123, -2.368261337751176310, -3.681124513963741851 ) ) ;
#421=LINE ( 'NONE', #7462, #13600 ) ;
#438=CARTESIAN_POINT ( 'NONE',  ( 0.000000000000000000, 0.000000000000000000, 3.469446951953614189E-15 ) ) ;
#445=ORIENTED_EDGE ( 'NONE', *, *, #12228, .T. ) ;
#456=CARTESIAN_POINT ( 'NONE',  ( 1.317756351988344177, -3.857995168970210997, -0.04852650426602210521 ) ) ;
#457=CARTESIAN_POINT ( 'NONE',  ( -1.654252653721913102, -3.663718938583020446, -0.01223254789874216215 ) ) ;
#474=CARTESIAN_POINT ( 'NONE',  ( -4.211140560182194292, -2.431303136016555122, -3.745885042887437510 ) ) ;
#475=CONICAL_SURFACE ( 'NONE', #1692, 5.560781378645573980, 1.221730476396046816 ) ;
#517=CARTESIAN_POINT ( 'NONE',  ( 4.175648173966053811, -2.207990556236549828, -3.469390959564066623 ) ) ;
#525=AXIS2_PLACEMENT_3D ( 'NONE', #2311, #1174, #12787 ) ;
#537=CARTESIAN_POINT ( 'NONE',  ( -1.144235203016679359, -3.958177651039093359, -0.09382832055446206632 ) ) ;
#550=CARTESIAN_POINT ( 'NONE',  ( 4.204015924366186319, -1.626724848190933104, -3.610627190413391752 ) ) ;
#566=CARTESIAN_POINT ( 'NONE',  ( 4.211399257449707889, -2.459727064652520223, -3.751161691472419513 ) ) ;
#610=EDGE_CURVE ( 'NONE', #5547, #3032, #3461, .T. ) ;
#631=CARTESIAN_POINT ( 'NONE',  ( 3.999999999999996447, 0.3987449864460007043, -0.01220643443059539826 ) ) ;
#636=DIRECTION ( 'NONE',  ( 1.000000000000000000, 0.000000000000000000, 0.000000000000000000 ) ) ;
#657=EDGE_LOOP ( 'NONE', ( #3709, #5297, #9603, #4959, #1883 ) ) ;
#685=ADVANCED_FACE ( 'NONE', ( #12725 ), #3271, .T. ) ;
#746=CARTESIAN_POINT ( 'NONE',  ( 0.000000000000000000, 0.000000000000000000, -25.03750572909317285 ) ) ;
#771=EDGE_LOOP ( 'NONE', ( #13238, #9884, #2856, #4385 ) ) ;
#772=DIRECTION ( 'NONE',  ( -1.000000000000000000, 0.000000000000000000, 0.000000000000000000 ) ) ;
#779=AXIS2_PLACEMENT_3D ( 'NONE', #4370, #14539, #5572 ) ;
#810=SHAPE_DEFINITION_REPRESENTATION ( #4040, #12767 ) ;
#846=CARTESIAN_POINT ( 'NONE',  ( 0.000000000000000000, 0.000000000000000000, -0.2800830152838856835 ) ) ;
#876=CARTESIAN_POINT ( 'NONE',  ( 3.999999999999998224, -1.677850389430954214, -3.535268758347605456 ) ) ;
#912=ORIENTED_EDGE ( 'NONE', *, *, #1117, .F. ) ;
#923=CARTESIAN_POINT ( 'NONE',  ( -0.5469614295415043959, 4.303013824935313814, -3.535263753545194287 ) ) ;
#945=DIRECTION ( 'NONE',  ( -1.000000000000000000, 0.000000000000000000, 0.000000000000000000 ) ) ;
#986=CONICAL_SURFACE ( 'NONE', #14304, 2.059999999999998721, 0.9599310885968738161 ) ;
#993=CARTESIAN_POINT ( 'NONE',  ( -2.725741868436042825, 3.045094352034018126, -3.220599429844233086 ) ) ;
#995=FACE_OUTER_BOUND ( 'NONE', #3641, .T. ) ;
#1021=ADVANCED_FACE ( 'NONE', ( #10349 ), #5198, .F. ) ;
#1023=CIRCLE ( 'NONE', #7051, 4.000000000000000000 ) ;
#1027=CARTESIAN_POINT ( 'NONE',  ( -3.999999999999996447, 2.309401076758498039, -5.000000000000000888 ) ) ;
#1053=CARTESIAN_POINT ( 'NONE',  ( 3.453038570459486589, 2.625189405339789062, -3.535263753543648413 ) ) ;
#1065=CARTESIAN_POINT ( 'NONE',  ( -4.024497503033713564, 2.323544716729485593, -3.572167766733750582 ) ) ;
#1075=CARTESIAN_POINT ( 'NONE',  ( 0.000000000000000000, 0.000000000000000000, -4.000000000000000000 ) ) ;
#1096=CARTESIAN_POINT ( 'NONE',  ( -3.999999999999998224, -2.472261339043344108, -3.687027428081193214 ) ) ;
#1111=CONICAL_SURFACE ( 'NONE', #3536, 4.000000000000000000, 0.8911886515913786111 ) ;
#1112=FACE_OUTER_BOUND ( 'NONE', #4539, .T. ) ;
#1117=EDGE_CURVE ( 'NONE', #7158, #3032, #9540, .T. ) ;
#1142=ORIENTED_EDGE ( 'NONE', *, *, #14457, .F. ) ;
#1147=CARTESIAN_POINT ( 'NONE',  ( -2.500000000000000888, 0.000000000000000000, -4.974599999999998801 ) ) ;
#1169=CARTESIAN_POINT ( 'NONE',  ( 0.000000000000000000, 4.618802153517009401, 0.000000000000000000 ) ) ;
#1174=DIRECTION ( 'NONE',  ( -0.000000000000000000, -0.000000000000000000, 1.000000000000000000 ) ) ;
#1177=CARTESIAN_POINT ( 'NONE',  ( -3.999999999999997335, 1.563622288139196126, -0.2253451193528282215 ) ) ;
#1185=ADVANCED_FACE ( 'NONE', ( #5031 ), #10720, .T. ) ;
#1199=CIRCLE ( 'NONE', #14053, 5.384454397937118664 ) ;
#1212=CARTESIAN_POINT ( 'NONE',  ( -4.236525694536555697, 2.416953475386462546, -3.751298745799836798 ) ) ;
#1229=FACE_OUTER_BOUND ( 'NONE', #8581, .T. ) ;
#1250=EDGE_CURVE ( 'NONE', #14881, #9830, #12087, .T. ) ;
#1252=CARTESIAN_POINT ( 'NONE',  ( 2.000000000000008882, 3.464101615137750390, 0.000000000000000000 ) ) ;
#1268=CARTESIAN_POINT ( 'NONE',  ( 2.742827927723424875, 3.035229711105287276, -3.433252694550964268 ) ) ;
#1273=EDGE_CURVE ( 'NONE', #11793, #11847, #5855, .T. ) ;
#1288=FACE_OUTER_BOUND ( 'NONE', #9095, .T. ) ;
#1320=CONICAL_SURFACE ( 'NONE', #2784, 2.500000000000000888, 0.9599310885968785900 ) ;
#1325=( BOUNDED_SURFACE ( )  B_SPLINE_SURFACE ( 3, 2, ( 
 ( #9176, #9022, #11558 ),
 ( #10248, #923, #7033 ),
 ( #13751, #5760, #2346 ),
 ( #993, #9935, #7957 ),
 ( #12600, #4631, #6963 ),
 ( #13903, #8114, #1212 ) ),
 .UNSPECIFIED., .F., .F., .F. ) 
 B_SPLINE_SURFACE_WITH_KNOTS ( ( 4, 2, 4 ),
 ( 3, 3 ),
 ( 0.02032853247518125531, 0.02278863295364820865, 0.02524873343211516200 ),
 ( 0.000000000000000000, 1.000000000000000000 ),
 .UNSPECIFIED. ) 
 GEOMETRIC_REPRESENTATION_ITEM ( )  RATIONAL_B_SPLINE_SURFACE ( (
 ( 1.000000000000000000, 0.8047781615896836271, 1.000000000000000000),
 ( 1.000000000000000000, 0.8123767586288900278, 1.000000000000000000),
 ( 1.000000000000000000, 0.8190662415564865517, 1.000000000000000000),
 ( 1.000000000000000000, 0.8192361015668555568, 1.000000000000000000),
 ( 1.000000000000000000, 0.8126135807104253317, 1.000000000000000000),
 ( 1.000000000000000000, 0.8047712338318587788, 1.000000000000000000) ) ) 
 REPRESENTATION_ITEM ( '' )  SURFACE ( )  );
#1326=CARTESIAN_POINT ( 'NONE',  ( -2.687328764639638212, 3.067272167851283982, -0.05923475698270262019 ) ) ;
#1327=CARTESIAN_POINT ( 'NONE',  ( -3.999999999999997335, 0.1981133338132461397, 2.803114366780232176E-15 ) ) ;
#1372=CARTESIAN_POINT ( 'NONE',  ( -3.999999999999996447, 1.539600717838995880, -3.300726591567077595 ) ) ;
#1378=EDGE_CURVE ( 'NONE', #11847, #14140, #14209, .T. ) ;
#1380=EDGE_CURVE ( 'NONE', #362, #8812, #1511, .T. ) ;
#1382=CARTESIAN_POINT ( 'NONE',  ( 2.449848172108559208, 3.432307619358739625, -3.503702292528904749 ) ) ;
#1415=CARTESIAN_POINT ( 'NONE',  ( 0.5449313310646723973, 4.304185902836962896, -3.316620875263447399 ) ) ;
#1416=FILL_AREA_STYLE_COLOUR ( '', #8948 ) ;
#1432=CARTESIAN_POINT ( 'NONE',  ( 0.5276280594147310099, -4.314175951381931995, -3.320322319201609584 ) ) ;
#1451=VECTOR ( 'NONE', #4253, 1000.000000000000114 ) ;
#1503=ORIENTED_EDGE ( 'NONE', *, *, #7814, .T. ) ;
#1510=CARTESIAN_POINT ( 'NONE',  ( -0.02448733951239507114, -4.877042772274745808, -3.751161874094030679 ) ) ;
#1511=B_SPLINE_CURVE_WITH_KNOTS ( 'NONE', 3,
 ( #2285, #12765, #10331, #2130, #7965, #12687 ),
 .UNSPECIFIED., .F., .F.,
 ( 4, 2, 4 ),
 ( 0.002452478801916377609, 0.003676905084148009151, 0.004901331366379640259 ),
 .UNSPECIFIED. ) ;
#1518=EDGE_CURVE ( 'NONE', #10622, #11548, #7942, .T. ) ;
#1537=DIRECTION ( 'NONE',  ( 0.000000000000000000, 0.000000000000000000, 1.000000000000000000 ) ) ;
#1560=DIRECTION ( 'NONE',  ( -1.000000000000000000, 0.000000000000000000, 0.000000000000000000 ) ) ;
#1564=CARTESIAN_POINT ( 'NONE',  ( 0.000000000000000000, 4.618802153517009401, -0.5000000000000004441 ) ) ;
#1587=CARTESIAN_POINT ( 'NONE',  ( 3.522875095019825764, -2.820352903225905372, -3.598441714920728618 ) ) ;
#1601=( GEOMETRIC_REPRESENTATION_CONTEXT ( 3 ) GLOBAL_UNCERTAINTY_ASSIGNED_CONTEXT ( ( #8799 ) ) GLOBAL_UNIT_ASSIGNED_CONTEXT ( ( #10701, #13060, #157 ) ) REPRESENTATION_CONTEXT ( 'NONE', 'WORKASPACE' ) );
#1606=CARTESIAN_POINT ( 'NONE',  ( -0.6448876103708539587, -4.246476118072355810, -0.2256878752776750596 ) ) ;
#1621=CARTESIAN_POINT ( 'NONE',  ( 0.000000000000000000, 0.000000000000000000, -5.000000000000000888 ) ) ;
#1650=B_SPLINE_CURVE_WITH_KNOTS ( 'NONE', 3,
 ( #4000, #2781, #10595, #7402, #9446 ),
 .UNSPECIFIED., .F., .F.,
 ( 4, 1, 4 ),
 ( 0.000000000000000000, 0.002309401076758502321, 0.004618802153517004641 ),
 .UNSPECIFIED. ) ;
#1656=CARTESIAN_POINT ( 'NONE',  ( -2.500000000000000444, 3.061616997868383634E-16, -5.000000000000000888 ) ) ;
#1658=CARTESIAN_POINT ( 'NONE',  ( -0.1750025118121570633, -4.719839900820638867, -3.469254087858256508 ) ) ;
#1662=ORIENTED_EDGE ( 'NONE', *, *, #14051, .T. ) ;
#1675=ADVANCED_BREP_SHAPE_REPRESENTATION ( '', ( #4390, #5108 ), #4118 ) ;
#1683=VERTEX_POINT ( 'NONE', #9303 ) ;
#1692=AXIS2_PLACEMENT_3D ( 'NONE', #1075, #3341, #10397 ) ;
#1701=CARTESIAN_POINT ( 'NONE',  ( 4.211405965630453885, 2.460463115436282600, -3.751298928144578770 ) ) ;
#1732=CYLINDRICAL_SURFACE ( 'NONE', #13949, 2.500000000000000444 ) ;
#1733=DIRECTION ( 'NONE',  ( -0.000000000000000000, 0.000000000000000000, -1.000000000000000000 ) ) ;
#1763=CARTESIAN_POINT ( 'NONE',  ( 3.999999999999996447, 0.1981133338132474442, 2.800855612254220445E-15 ) ) ;
#1789=CARTESIAN_POINT ( 'NONE',  ( 5.560781378645575757, 0.000000000000000000, -4.000000000000000000 ) ) ;
#1798=CARTESIAN_POINT ( 'NONE',  ( 4.938688511801393915E-15, 4.736522675502336632, -3.681124513963741851 ) ) ;
#1804=ORIENTED_EDGE ( 'NONE', *, *, #12150, .F. ) ;
#1812=EDGE_LOOP ( 'NONE', ( #10508, #10733, #3910, #9380 ) ) ;
#1814=CARTESIAN_POINT ( 'NONE',  ( 3.355112389629170355, -2.681727112203167174, -0.2256878752776754760 ) ) ;
#1859=CARTESIAN_POINT ( 'NONE',  ( -2.742827927723403114, -3.035229711105392081, -3.433252694550782191 ) ) ;
#1860=ORIENTED_EDGE ( 'NONE', *, *, #2490, .T. ) ;
#1863=CARTESIAN_POINT ( 'NONE',  ( 2.499999999999999556, 0.000000000000000000, 3.469446951953614189E-15 ) ) ;
#1883=ORIENTED_EDGE ( 'NONE', *, *, #1117, .T. ) ;
#1885=CLOSED_SHELL ( 'NONE', ( #10718, #5433, #13573, #26, #11639, #6471, #2390, #13893, #5265, #5965, #13219, #5173, #1185, #2571, #6931, #10006, #8198, #14000, #6423, #685, #4106, #2133, #10786, #13308, #11776, #7859, #3694, #14943, #12061, #7453, #1021, #6109 ) ) ;
#1909=CARTESIAN_POINT ( 'NONE',  ( -4.211140560182194292, 2.431303136016534250, -3.745885042887433958 ) ) ;
#1933=CIRCLE ( 'NONE', #11654, 2.500000000000000888 ) ;
#1934=CIRCLE ( 'NONE', #10177, 2.500000000000000444 ) ;
#1970=DIRECTION ( 'NONE',  ( 1.000000000000000000, 0.000000000000000000, 0.000000000000000000 ) ) ;
#1974=CARTESIAN_POINT ( 'NONE',  ( 0.000000000000000000, 0.000000000000000000, 0.000000000000000000 ) ) ;
#2015=ORIENTED_EDGE ( 'NONE', *, *, #9266, .F. ) ;
#2025=ORIENTED_EDGE ( 'NONE', *, *, #8699, .F. ) ;
#2026=EDGE_CURVE ( 'NONE', #8852, #9388, #6577, .T. ) ;
#2027=VECTOR ( 'NONE', #13115, 1000.000000000000000 ) ;
#2028=DIRECTION ( 'NONE',  ( 0.000000000000000000, 0.000000000000000000, -1.000000000000000000 ) ) ;
#2047=DIRECTION ( 'NONE',  ( -0.000000000000000000, 0.000000000000000000, -1.000000000000000000 ) ) ;
#2058=B_SPLINE_CURVE_WITH_KNOTS ( 'NONE', 3,
 ( #11031, #11871, #10801, #550, #4966, #9642 ),
 .UNSPECIFIED., .F., .F.,
 ( 4, 2, 4 ),
 ( 0.002452478801916362864, 0.003676905084148002212, 0.004901331366379641993 ),
 .UNSPECIFIED. ) ;
#2064=CIRCLE ( 'NONE', #6658, 5.560781378645573980 ) ;
#2079=B_SPLINE_CURVE_WITH_KNOTS ( 'NONE', 3,
 ( #12833, #8352, #11852, #7273, #3808, #2503 ),
 .UNSPECIFIED., .F., .F.,
 ( 4, 2, 4 ),
 ( 0.003358874760055550589, 0.004541967308452098118, 0.005725059856848646080 ),
 .UNSPECIFIED. ) ;
#2083=CARTESIAN_POINT ( 'NONE',  ( 0.1410422978106151692, -4.700232962125109104, -3.687027686973631369 ) ) ;
#2096=ORIENTED_EDGE ( 'NONE', *, *, #9708, .T. ) ;
#2117=DIRECTION ( 'NONE',  ( 0.000000000000000000, -0.000000000000000000, 1.000000000000000000 ) ) ;
#2130=CARTESIAN_POINT ( 'NONE',  ( -4.204015924366186319, 1.626724848190920891, -3.610627190413389975 ) ) ;
#2132=CARTESIAN_POINT ( 'NONE',  ( -4.197393957002300446, -0.8151795401431412014, -3.503767560748934251 ) ) ;
#2133=ADVANCED_FACE ( 'NONE', ( #12504 ), #7908, .T. ) ;
#2141=CARTESIAN_POINT ( 'NONE',  ( 0.000000000000000000, 0.000000000000000000, -4.000000000000000000 ) ) ;
#2156=ORIENTED_EDGE ( 'NONE', *, *, #5373, .F. ) ;
#2172=DIRECTION ( 'NONE',  ( -1.000000000000000000, 0.000000000000000000, 0.000000000000000000 ) ) ;
#2181=DIRECTION ( 'NONE',  ( 0.000000000000000000, 0.000000000000000000, -1.000000000000000000 ) ) ;
#2193=DIRECTION ( 'NONE',  ( -1.000000000000000000, 0.000000000000000000, 0.000000000000000000 ) ) ;
#2203=CIRCLE ( 'NONE', #10685, 2.100000000000000089 ) ;
#2227=ORIENTED_EDGE ( 'NONE', *, *, #9425, .T. ) ;
#2228=DIRECTION ( 'NONE',  ( 0.000000000000000000, 0.000000000000000000, -1.000000000000000000 ) ) ;
#2236=ORIENTED_EDGE ( 'NONE', *, *, #14652, .F. ) ;
#2247=DIRECTION ( 'NONE',  ( -1.000000000000000000, 0.000000000000000000, 0.000000000000000000 ) ) ;
#2249=CARTESIAN_POINT ( 'NONE',  ( -3.999999999999997335, -1.942223658245637807, -0.3516579909967631479 ) ) ;
#2273=ORIENTED_EDGE ( 'NONE', *, *, #2763, .F. ) ;
#2285=CARTESIAN_POINT ( 'NONE',  ( -4.197393957002300446, -7.680494662014190109E-14, -3.503767560748928922 ) ) ;
#2295=CARTESIAN_POINT ( 'NONE',  ( -3.999999999999998224, 2.511478553582034312, -3.469254451724766319 ) ) ;
#2311=CARTESIAN_POINT ( 'NONE',  ( 0.000000000000000000, 0.000000000000000000, -0.3080913168122742518 ) ) ;
#2326=VERTEX_POINT ( 'NONE', #5270 ) ;
#2327=B_SPLINE_CURVE_WITH_KNOTS ( 'NONE', 3,
 ( #4036, #7359, #1606, #537, #5167, #457, #5089, #11943 ),
 .UNSPECIFIED., .F., .F.,
 ( 4, 2, 2, 4 ),
 ( 2.465131517396147670E-07, 0.001183067374689869729, 0.001774477805458935225, 0.002365888236228000721 ),
 .UNSPECIFIED. ) ;
#2330=FACE_OUTER_BOUND ( 'NONE', #5410, .T. ) ;
#2336=CARTESIAN_POINT ( 'NONE',  ( 4.024499207728847949, 2.323545700935682579, -3.572172305156875005 ) ) ;
#2346=CARTESIAN_POINT ( 'NONE',  ( -1.360585162435266282, 4.061296242128070944, -3.505054077164856619 ) ) ;
#2356=ORIENTED_EDGE ( 'NONE', *, *, #9588, .T. ) ;
#2358=ORIENTED_EDGE ( 'NONE', *, *, #5046, .F. ) ;
#2364=DIRECTION ( 'NONE',  ( 1.000000000000000000, 0.000000000000000000, 0.000000000000000000 ) ) ;
#2368=DIRECTION ( 'NONE',  ( 0.000000000000000000, -1.000000000000000000, 0.000000000000000000 ) ) ;
#2370=CONICAL_SURFACE ( 'NONE', #14495, 5.560781378645573980, 1.221730476396046816 ) ;
#2378=CARTESIAN_POINT ( 'NONE',  ( -3.999999999999997335, 0.3987449864459985394, -0.01220643443059497325 ) ) ;
#2390=ADVANCED_FACE ( 'NONE', ( #13468 ), #5341, .F. ) ;
#2393=CARTESIAN_POINT ( 'NONE',  ( 3.540020015735463321, 2.810662092923963407, -3.602146406945750279 ) ) ;
#2395=CARTESIAN_POINT ( 'NONE',  ( 4.154306624730760511, -2.398490048084971349, -3.721999068284304713 ) ) ;
#2445=DIRECTION ( 'NONE',  ( 0.000000000000000000, 0.000000000000000000, 1.000000000000000000 ) ) ;
#2450=B_SPLINE_CURVE_WITH_KNOTS ( 'NONE', 3,
 ( #9072, #2249, #12728, #4675, #6864, #3613 ),
 .UNSPECIFIED., .F., .F.,
 ( 4, 2, 4 ),
 ( 0.003358874760055547120, 0.004541967308452095516, 0.005725059856848643478 ),
 .UNSPECIFIED. ) ;
#2453=DIRECTION ( 'NONE',  ( -0.000000000000000000, -0.000000000000000000, 1.000000000000000000 ) ) ;
#2490=EDGE_CURVE ( 'NONE', #14675, #13811, #5498, .T. ) ;
#2503=CARTESIAN_POINT ( 'NONE',  ( 3.999999999999996447, 0.000000000000000000, 0.000000000000000000 ) ) ;
#2507=CARTESIAN_POINT ( 'NONE',  ( 4.211140560182194292, 2.431303136016534250, -3.745885042887433958 ) ) ;
#2509=DIRECTION ( 'NONE',  ( -0.9396926207859138680, 0.000000000000000000, -0.3420201433256536139 ) ) ;
#2513=CARTESIAN_POINT ( 'NONE',  ( -4.197477534772231067, 0.8522413273724359639, -3.505042416683227025 ) ) ;
#2519=CARTESIAN_POINT ( 'NONE',  ( 1.312671235360371558, 3.860931062424218574, -0.05923475698270420919 ) ) ;
#2530=VERTEX_POINT ( 'NONE', #4358 ) ;
#2554=LINE ( 'NONE', #9232, #7528 ) ;
#2556=SURFACE_STYLE_USAGE ( .BOTH. , #194 ) ;
#2568=VERTEX_POINT ( 'NONE', #11420 ) ;
#2569=AXIS2_PLACEMENT_3D ( 'NONE', #11362, #10434, #14857 ) ;
#2571=ADVANCED_FACE ( 'NONE', ( #14913, #7835 ), #6920, .F. ) ;
#2615=APPLICATION_CONTEXT ( 'automotive_design' ) ;
#2623=DIRECTION ( 'NONE',  ( -0.8191520442889875797, 1.003171929053519570E-16, 0.5735764363510522656 ) ) ;
#2624=CARTESIAN_POINT ( 'NONE',  ( -0.02511973781850361173, 4.877415612947412882, -3.751298745799841239 ) ) ;
#2641=CARTESIAN_POINT ( 'NONE',  ( 1.360585162435297590, -4.061296242128142886, -3.505054077164885484 ) ) ;
#2666=AXIS2_PLACEMENT_3D ( 'NONE', #8817, #12255, #636 ) ;
#2694=EDGE_CURVE ( 'NONE', #5971, #7436, #3726, .T. ) ;
#2697=ORIENTED_EDGE ( 'NONE', *, *, #14317, .T. ) ;
#2763=EDGE_CURVE ( 'NONE', #4112, #1683, #14226, .T. ) ;
#2781=CARTESIAN_POINT ( 'NONE',  ( 0.6666666666666654084, -4.233901974057272533, -3.300726591567086921 ) ) ;
#2784=AXIS2_PLACEMENT_3D ( 'NONE', #11335, #11404, #9186 ) ;
#2786=ORIENTED_EDGE ( 'NONE', *, *, #3759, .T. ) ;
#2790=B_SPLINE_CURVE_WITH_KNOTS ( 'NONE', 3,
 ( #7719, #8932, #1814, #12362, #7571, #14731, #11001, #9850 ),
 .UNSPECIFIED., .F., .F.,
 ( 4, 2, 2, 4 ),
 ( 2.465131517120941901E-07, 0.001183067374689838070, 0.001774477805458900747, 0.002365888236227963858 ),
 .UNSPECIFIED. ) ;
#2803=CIRCLE ( 'NONE', #5934, 0.5155456020628804703 ) ;
#2831=FACE_OUTER_BOUND ( 'NONE', #11343, .T. ) ;
#2842=CARTESIAN_POINT ( 'NONE',  ( 0.000000000000000000, 0.000000000000000000, -5.000000000000000888 ) ) ;
#2847=CARTESIAN_POINT ( 'NONE',  ( 0.000000000000000000, 0.000000000000000000, -4.694516984716113228 ) ) ;
#2852=CARTESIAN_POINT ( 'NONE',  ( 0.6810597143197147929, 4.461075778259437463, -3.598441714920656676 ) ) ;
#2855=VERTEX_POINT ( 'NONE', #4109 ) ;
#2856=ORIENTED_EDGE ( 'NONE', *, *, #12772, .T. ) ;
#2867=CARTESIAN_POINT ( 'NONE',  ( 1.257172072275600794, -3.892973519171010643, -3.433252694550598783 ) ) ;
#2868=( BOUNDED_SURFACE ( )  B_SPLINE_SURFACE ( 3, 2, ( 
 ( #5884, #9301, #13959 ),
 ( #3552, #1053, #2393 ),
 ( #7011, #1268, #123 ),
 ( #9376, #13107, #4914 ),
 ( #1415, #11750, #2852 ),
 ( #6184, #5054, #2624 ) ),
 .UNSPECIFIED., .F., .F., .F. ) 
 B_SPLINE_SURFACE_WITH_KNOTS ( ( 4, 2, 4 ),
 ( 3, 3 ),
 ( 0.02032853247518126225, 0.02278863295364821212, 0.02524873343211516200 ),
 ( 0.000000000000000000, 1.000000000000000000 ),
 .UNSPECIFIED. ) 
 GEOMETRIC_REPRESENTATION_ITEM ( )  RATIONAL_B_SPLINE_SURFACE ( (
 ( 1.000000000000000000, 0.8047781615896835161, 1.000000000000000000),
 ( 1.000000000000000000, 0.8123767586289261100, 1.000000000000000000),
 ( 1.000000000000000000, 0.8190662415564383680, 1.000000000000000000),
 ( 1.000000000000000000, 0.8192361015669021862, 1.000000000000000000),
 ( 1.000000000000000000, 0.8126135807103909148, 1.000000000000000000),
 ( 1.000000000000000000, 0.8047712338318580017, 1.000000000000000000) ) ) 
 REPRESENTATION_ITEM ( '' )  SURFACE ( )  );
#2915=AXIS2_PLACEMENT_3D ( 'NONE', #3829, #7223, #6229 ) ;
#2917=ORIENTED_EDGE ( 'NONE', *, *, #9425, .F. ) ;
#2927=PRODUCT_CONTEXT ( 'NONE', #3784, 'mechanical' ) ;
#2945=EDGE_CURVE ( 'NONE', #9923, #1683, #4772, .T. ) ;
#2971=CARTESIAN_POINT ( 'NONE',  ( 4.197393957002300446, 0.8151795401431369825, -3.503767560748934251 ) ) ;
#2992=CARTESIAN_POINT ( 'NONE',  ( 3.999999999999998224, -0.8732470631450011123, -3.223155494240760977 ) ) ;
#2994=ORIENTED_EDGE ( 'NONE', *, *, #14721, .F. ) ;
#2995=VERTEX_POINT ( 'NONE', #5693 ) ;
#2996=DIRECTION ( 'NONE',  ( 0.8660254037844379305, 0.5000000000000013323, 0.000000000000000000 ) ) ;
#3023=EDGE_CURVE ( 'NONE', #12909, #2568, #5001, .T. ) ;
#3032=VERTEX_POINT ( 'NONE', #8623 ) ;
#3055=CARTESIAN_POINT ( 'NONE',  ( 4.211140560182194292, -2.431303136016555122, -3.745885042887437510 ) ) ;
#3068=CARTESIAN_POINT ( 'NONE',  ( 3.999999999999996447, 2.309401076758498039, -3.433295621305378020 ) ) ;
#3097=CARTESIAN_POINT ( 'NONE',  ( 0.000000000000000000, 4.618802153517009401, -5.000000000000000888 ) ) ;
#3102=EDGE_CURVE ( 'NONE', #7535, #5322, #5894, .T. ) ;
#3122=CARTESIAN_POINT ( 'NONE',  ( 0.000000000000000000, 0.000000000000000000, -0.2800830152838856835 ) ) ;
#3128=B_SPLINE_CURVE_WITH_KNOTS ( 'NONE', 3,
 ( #9703, #10857, #456, #11942, #5026, #11791 ),
 .UNSPECIFIED., .F., .F.,
 ( 4, 2, 4 ),
 ( 0.002365888236227963858, 0.003551327329835074140, 0.004736766423442183988 ),
 .UNSPECIFIED. ) ;
#3131=CARTESIAN_POINT ( 'NONE',  ( -2.805705207896067144, 3.226868319750154868, -3.503898532754365025 ) ) ;
#3133=B_SPLINE_CURVE_WITH_KNOTS ( 'NONE', 3,
 ( #11778, #1372, #5984, #10620, #4495 ),
 .UNSPECIFIED., .F., .F.,
 ( 4, 1, 4 ),
 ( 0.000000000000000000, 0.002309401076758505790, 0.004618802153517011580 ),
 .UNSPECIFIED. ) ;
#3137=VERTEX_POINT ( 'NONE', #11909 ) ;
#3140=ORIENTED_EDGE ( 'NONE', *, *, #6417, .T. ) ;
#3197=CARTESIAN_POINT ( 'NONE',  ( 2.805705207896068920, -3.226868319750169078, -3.503898532754369022 ) ) ;
#3200=DIRECTION ( 'NONE',  ( 1.224646799147353207E-16, 1.000000000000000000, 0.000000000000000000 ) ) ;
#3204=CARTESIAN_POINT ( 'NONE',  ( 2.000000000000008882, -3.464101615137750390, 0.000000000000000000 ) ) ;
#3224=ORIENTED_EDGE ( 'NONE', *, *, #3759, .F. ) ;
#3253=CARTESIAN_POINT ( 'NONE',  ( 3.999999999999996447, -2.309401076758518911, -3.433295621305385126 ) ) ;
#3259=CARTESIAN_POINT ( 'NONE',  ( -4.154094228333540251, 2.398367420968064323, -3.721909803043256915 ) ) ;
#3266=FACE_OUTER_BOUND ( 'NONE', #1812, .T. ) ;
#3271=CONICAL_SURFACE ( 'NONE', #13213, 4.000000000000000000, 0.8911886515913786111 ) ;
#3281=AXIS2_PLACEMENT_3D ( 'NONE', #14701, #4447, #9058 ) ;
#3303=CARTESIAN_POINT ( 'NONE',  ( -1.287237434361998778, -3.875615274276856592, -3.430618716626631759 ) ) ;
#3320=VECTOR ( 'NONE', #6649, 1000.000000000000000 ) ;
#3335=CARTESIAN_POINT ( 'NONE',  ( 0.000000000000000000, 0.000000000000000000, -5.000000000000000888 ) ) ;
#3339=DIRECTION ( 'NONE',  ( 1.000000000000000000, 0.000000000000000000, 0.000000000000000000 ) ) ;
#3341=DIRECTION ( 'NONE',  ( 0.000000000000000000, 0.000000000000000000, -1.000000000000000000 ) ) ;
#3357=CARTESIAN_POINT ( 'NONE',  ( -3.999999999999998224, -1.680117682357869624, -3.316611593219199072 ) ) ;
#3374=ORIENTED_EDGE ( 'NONE', *, *, #13577, .F. ) ;
#3413=EDGE_CURVE ( 'NONE', #3032, #5002, #2450, .T. ) ;
#3415=CARTESIAN_POINT ( 'NONE',  ( -2.000000000000008882, 3.464101615137750390, 0.000000000000000000 ) ) ;
#3426=ORIENTED_EDGE ( 'NONE', *, *, #1273, .T. ) ;
#3432=CARTESIAN_POINT ( 'NONE',  ( 0.6920835326022575229, 4.454600218803879130, -3.597382984111580306 ) ) ;
#3455=CARTESIAN_POINT ( 'NONE',  ( -3.999999999999996447, 0.9868501483902569760, -0.09357334158579228012 ) ) ;
#3461=LINE ( 'NONE', #3612, #12236 ) ;
#3475=CARTESIAN_POINT ( 'NONE',  ( 4.024499207728847061, -2.323545700935702119, -3.572172305156873673 ) ) ;
#3479=ORIENTED_EDGE ( 'NONE', *, *, #11172, .T. ) ;
#3485=VECTOR ( 'NONE', #5617, 1000.000000000000000 ) ;
#3487=DIRECTION ( 'NONE',  ( -0.000000000000000000, 0.000000000000000000, -1.000000000000000000 ) ) ;
#3517=CARTESIAN_POINT ( 'NONE',  ( -3.999999999999626965, -0.8232339106132875450, -3.430630286862371925 ) ) ;
#3536=AXIS2_PLACEMENT_3D ( 'NONE', #5255, #13519, #13234 ) ;
#3552=CARTESIAN_POINT ( 'NONE',  ( 3.472371940586087558, 2.614027278893122475, -3.320322319201942207 ) ) ;
#3580=FILL_AREA_STYLE_COLOUR ( '', #6425 ) ;
#3591=ORIENTED_EDGE ( 'NONE', *, *, #12772, .F. ) ;
#3593=CARTESIAN_POINT ( 'NONE',  ( -3.679171394226030678, -2.494631558665843407, -0.3503314178412529345 ) ) ;
#3603=CARTESIAN_POINT ( 'NONE',  ( 0.000000000000000000, 0.000000000000000000, 3.469446951953614189E-15 ) ) ;
#3612=CARTESIAN_POINT ( 'NONE',  ( -3.999999999999996447, -2.309401076758511806, -5.000000000000000888 ) ) ;
#3613=CARTESIAN_POINT ( 'NONE',  ( -3.999999999999996447, 0.000000000000000000, 0.000000000000000000 ) ) ;
#3641=EDGE_LOOP ( 'NONE', ( #7875, #11828, #3426, #14355, #4996, #3479, #14033 ) ) ;
#3650=CARTESIAN_POINT ( 'NONE',  ( 1.843833675287984673E-15, -4.647091401871394467, -3.572172305156880778 ) ) ;
#3677=EDGE_LOOP ( 'NONE', ( #13640, #4257, #11348, #3140 ) ) ;
#3694=ADVANCED_FACE ( 'NONE', ( #12407 ), #9071, .F. ) ;
#3698=CARTESIAN_POINT ( 'NONE',  ( 0.000000000000000000, 0.000000000000000000, 0.000000000000000000 ) ) ;
#3699=SURFACE_STYLE_FILL_AREA ( #10666 ) ;
#3709=ORIENTED_EDGE ( 'NONE', *, *, #610, .F. ) ;
#3726=B_SPLINE_CURVE_WITH_KNOTS ( 'NONE', 3,
 ( #5932, #10571, #4802, #7140, #2519, #9415, #13007, #14064 ),
 .UNSPECIFIED., .F., .F.,
 ( 4, 2, 2, 4 ),
 ( 2.465131517060789857E-07, 0.001183067374689849563, 0.001774477805458922215, 0.002365888236227995083 ),
 .UNSPECIFIED. ) ;
#3747=CARTESIAN_POINT ( 'NONE',  ( 3.999999999999996447, 2.309401076758498039, -3.433295621305378020 ) ) ;
#3756=DIRECTION ( 'NONE',  ( -0.000000000000000000, -0.000000000000000000, 1.000000000000000000 ) ) ;
#3759=EDGE_CURVE ( 'NONE', #9923, #2530, #13174, .T. ) ;
#3780=SHAPE_REPRESENTATION_RELATIONSHIP ( 'NONE' , 'NONE' ,  #12767, #1675 ) ;
#3784=APPLICATION_CONTEXT ( 'automotive_design' ) ;
#3797=CARTESIAN_POINT ( 'NONE',  ( 0.6640947660592916302, -4.471078309994156896, -3.602146406945703649 ) ) ;
#3805=AXIS2_PLACEMENT_3D ( 'NONE', #2842, #7759, #6387 ) ;
#3808=CARTESIAN_POINT ( 'NONE',  ( 3.999999999999996447, -0.3979232138631224602, 2.803679055411734122E-15 ) ) ;
#3829=CARTESIAN_POINT ( 'NONE',  ( 0.000000000000000000, 0.000000000000000000, 0.000000000000000000 ) ) ;
#3853=DIRECTION ( 'NONE',  ( -0.000000000000000000, 0.000000000000000000, -1.000000000000000000 ) ) ;
#3859=ORIENTED_EDGE ( 'NONE', *, *, #5983, .F. ) ;
#3870=ORIENTED_EDGE ( 'NONE', *, *, #5046, .T. ) ;
#3910=ORIENTED_EDGE ( 'NONE', *, *, #2026, .F. ) ;
#3917=DIRECTION ( 'NONE',  ( 0.5000000000000013323, -0.8660254037844379305, 0.000000000000000000 ) ) ;
#3933=DIRECTION ( 'NONE',  ( -1.000000000000000000, 0.000000000000000000, 0.000000000000000000 ) ) ;
#3939=EDGE_CURVE ( 'NONE', #10230, #9910, #5523, .T. ) ;
#3941=DIRECTION ( 'NONE',  ( -1.000000000000000000, 0.000000000000000000, 0.000000000000000000 ) ) ;
#3971=CARTESIAN_POINT ( 'NONE',  ( 0.000000000000000000, -4.618802153517023612, -3.433295621305388678 ) ) ;
#3978=VECTOR ( 'NONE', #5191, 1000.000000000000000 ) ;
#3980=CARTESIAN_POINT ( 'NONE',  ( 2.100000000000000089, 0.000000000000000000, -5.000000000000000888 ) ) ;
#4000=CARTESIAN_POINT ( 'NONE',  ( 0.000000000000000000, -4.618802153517023612, -3.433295621305388678 ) ) ;
#4004=AXIS2_PLACEMENT_3D ( 'NONE', #12435, #2028, #13729 ) ;
#4016=CARTESIAN_POINT ( 'NONE',  ( -4.024497503033713564, -2.323544716729502468, -3.572167766733754135 ) ) ;
#4036=CARTESIAN_POINT ( 'NONE',  ( -2.775557561562891351E-14, -4.618802153517009401, -0.5000000000000004441 ) ) ;
#4040=PRODUCT_DEFINITION_SHAPE ( 'NONE', 'NONE',  #14333 ) ;
#4052=DIRECTION ( 'NONE',  ( 0.000000000000000000, -0.000000000000000000, 1.000000000000000000 ) ) ;
#4065=PRODUCT_DEFINITION_CONTEXT ( 'detailed design', #2615, 'design' ) ;
#4096=LINE ( 'NONE', #4178, #1451 ) ;
#4106=ADVANCED_FACE ( 'NONE', ( #12385 ), #1111, .T. ) ;
#4109=CARTESIAN_POINT ( 'NONE',  ( 3.999999999999996447, 2.309401076758511806, -0.5000000000000004441 ) ) ;
#4111=CARTESIAN_POINT ( 'NONE',  ( -4.211140560182194292, -2.431303136016555122, -3.745885042887437510 ) ) ;
#4112=VERTEX_POINT ( 'NONE', #7740 ) ;
#4115=CARTESIAN_POINT ( 'NONE',  ( 3.999999999999997335, 1.563622288139205230, -0.2253451193528305807 ) ) ;
#4118=( GEOMETRIC_REPRESENTATION_CONTEXT ( 3 ) GLOBAL_UNCERTAINTY_ASSIGNED_CONTEXT ( ( #10881 ) ) GLOBAL_UNIT_ASSIGNED_CONTEXT ( ( #11982, #12808, #7171 ) ) REPRESENTATION_CONTEXT ( 'NONE', 'WORKASPACE' ) );
#4137=CARTESIAN_POINT ( 'NONE',  ( 3.999999999999998224, -2.471525695159797031, -3.686886880705772640 ) ) ;
#4143=CARTESIAN_POINT ( 'NONE',  ( -3.540020015735788395, -2.810662092924504751, -3.602146406945951451 ) ) ;
#4168=DIRECTION ( 'NONE',  ( 1.000000000000000000, 0.000000000000000000, 0.000000000000000000 ) ) ;
#4170=PRODUCT ( 'hex flange nut gradea_iso_ISO - 4161 - M5 - N', 'hex flange nut gradea_iso_ISO - 4161 - M5 - N', '', ( #2927 ) ) ;
#4178=CARTESIAN_POINT ( 'NONE',  ( -2.500000000000000888, 0.000000000000000000, -4.974599999999998801 ) ) ;
#4185=B_SPLINE_CURVE_WITH_KNOTS ( 'NONE', 3,
 ( #9142, #6706, #11356, #11593, #9288 ),
 .UNSPECIFIED., .F., .F.,
 ( 4, 1, 4 ),
 ( 0.000000000000000000, 0.002309401076758506657, 0.004618802153517013315 ),
 .UNSPECIFIED. ) ;
#4187=EDGE_CURVE ( 'NONE', #14140, #362, #7310, .T. ) ;
#4189=LINE ( 'NONE', #13438, #11779 ) ;
#4217=DIRECTION ( 'NONE',  ( -0.000000000000000000, -0.000000000000000000, 1.000000000000000000 ) ) ;
#4218=EDGE_CURVE ( 'NONE', #5448, #6726, #2803, .T. ) ;
#4245=DIRECTION ( 'NONE',  ( -0.000000000000000000, -0.000000000000000000, 1.000000000000000000 ) ) ;
#4253=DIRECTION ( 'NONE',  ( -0.8191520442889902442, 0.000000000000000000, -0.5735764363510482688 ) ) ;
#4257=ORIENTED_EDGE ( 'NONE', *, *, #9708, .F. ) ;
#4258=VECTOR ( 'NONE', #2509, 1000.000000000000227 ) ;
#4264=EDGE_CURVE ( 'NONE', #4112, #13996, #7900, .T. ) ;
#4300=CARTESIAN_POINT ( 'NONE',  ( -1.390230914382368121, -4.043987460488665420, -3.502507215260525442 ) ) ;
#4303=FACE_OUTER_BOUND ( 'NONE', #7574, .T. ) ;
#4329=EDGE_CURVE ( 'NONE', #2995, #7535, #2079, .T. ) ;
#4332=CARTESIAN_POINT ( 'NONE',  ( -4.211140560182194292, 2.431303136016534250, -3.745885042887433958 ) ) ;
#4348=ORIENTED_EDGE ( 'NONE', *, *, #10741, .T. ) ;
#4358=CARTESIAN_POINT ( 'NONE',  ( 2.100000000000000089, 0.000000000000000000, -4.694516984716113228 ) ) ;
#4362=CARTESIAN_POINT ( 'NONE',  ( 4.197310751797290962, 0.8178363989516218568, -3.502498386812445297 ) ) ;
#4370=CARTESIAN_POINT ( 'NONE',  ( 0.000000000000000000, 4.618802153517009401, -5.000000000000000888 ) ) ;
#4385=ORIENTED_EDGE ( 'NONE', *, *, #3023, .F. ) ;
#4390=MANIFOLD_SOLID_BREP ( 'EndChamfer', #1885 ) ;
#4408=EDGE_CURVE ( 'NONE', #10917, #11847, #5147, .T. ) ;
#4423=CARTESIAN_POINT ( 'NONE',  ( 4.203833317240876610, 1.627343821129586532, -3.597273115243891262 ) ) ;
#4443=AXIS2_PLACEMENT_3D ( 'NONE', #6309, #4217, #8827 ) ;
#4447=DIRECTION ( 'NONE',  ( -0.000000000000000000, -0.000000000000000000, 1.000000000000000000 ) ) ;
#4448=DIRECTION ( 'NONE',  ( -1.000000000000000000, 0.000000000000000000, 0.000000000000000000 ) ) ;
#4495=CARTESIAN_POINT ( 'NONE',  ( -3.999999999999996447, -2.309401076758511806, -3.433295621305381573 ) ) ;
#4502=CARTESIAN_POINT ( 'NONE',  ( -4.203833317240876610, -1.627343821129593415, -3.597273115243891262 ) ) ;
#4518=CARTESIAN_POINT ( 'NONE',  ( 3.999999999999996447, -1.539600717839016308, -3.300726591567079371 ) ) ;
#4539=EDGE_LOOP ( 'NONE', ( #6209, #9809, #8776, #8648 ) ) ;
#4551=EDGE_LOOP ( 'NONE', ( #2096, #9995 ) ) ;
#4552=EDGE_CURVE ( 'NONE', #8812, #13753, #243, .T. ) ;
#4571=CARTESIAN_POINT ( 'NONE',  ( 0.000000000000000000, 4.862606272033088928, -3.745885042887437510 ) ) ;
#4572=CARTESIAN_POINT ( 'NONE',  ( 3.349226789952651995, 2.685125164760731487, -0.2236248678334764872 ) ) ;
#4589=EDGE_CURVE ( 'NONE', #10622, #12909, #7411, .T. ) ;
#4593=DIRECTION ( 'NONE',  ( -0.000000000000000000, -0.000000000000000000, 1.000000000000000000 ) ) ;
#4618=EDGE_CURVE ( 'NONE', #5322, #7158, #12758, .T. ) ;
#4631=CARTESIAN_POINT ( 'NONE',  ( -3.436319922987371989, 2.634841920960311334, -3.531542292954659157 ) ) ;
#4642=ORIENTED_EDGE ( 'NONE', *, *, #2490, .F. ) ;
#4675=CARTESIAN_POINT ( 'NONE',  ( -3.999999999999997335, -0.7890432684750902093, -0.04868663549882015773 ) ) ;
#4718=SURFACE_STYLE_FILL_AREA ( #76 ) ;
#4727=CARTESIAN_POINT ( 'NONE',  ( 2.000000000000008882, 3.464101615137750390, 0.000000000000000000 ) ) ;
#4738=CARTESIAN_POINT ( 'NONE',  ( -3.349226789952651995, -2.685125164760743033, -0.2236248678334835094 ) ) ;
#4747=CARTESIAN_POINT ( 'NONE',  ( -3.999999999999996447, 2.309401076758498039, -0.4999999999999935052 ) ) ;
#4770=CARTESIAN_POINT ( 'NONE',  ( 3.999999999999996447, 2.309401076758498039, -3.433295621305378020 ) ) ;
#4772=LINE ( 'NONE', #11248, #3485 ) ;
#4795=DIRECTION ( 'NONE',  ( -0.000000000000000000, -0.000000000000000000, 1.000000000000000000 ) ) ;
#4798=CARTESIAN_POINT ( 'NONE',  ( 2.500000000000000888, 3.061616997868384127E-16, -4.974599999999998801 ) ) ;
#4801=B_SPLINE_CURVE_WITH_KNOTS ( 'NONE', 3,
 ( #4770, #13890, #2336, #10530, #134, #10455 ),
 .UNSPECIFIED., .F., .F.,
 ( 4, 2, 4 ),
 ( 0.000000000000000000, 0.0002095117440864783663, 0.0004190234881729567326 ),
 .UNSPECIFIED. ) ;
#4802=CARTESIAN_POINT ( 'NONE',  ( 0.6448876103708347518, 4.246476118072353145, -0.2256878752776711461 ) ) ;
#4807=DIRECTION ( 'NONE',  ( 0.5000000000000022204, 0.8660254037844374864, -0.000000000000000000 ) ) ;
#4814=CARTESIAN_POINT ( 'NONE',  ( 0.000000000000000000, 0.000000000000000000, -0.3080913168122742518 ) ) ;
#4846=CIRCLE ( 'NONE', #12125, 2.100000000000000089 ) ;
#4847=CARTESIAN_POINT ( 'NONE',  ( 0.000000000000000000, 0.000000000000000000, -4.484454397937119197 ) ) ;
#4864=SURFACE_SIDE_STYLE ('',( #4718 ) ) ;
#4886=CARTESIAN_POINT ( 'NONE',  ( 4.000000000000000000, -1.062518129035794345E-14, -3.142992957459236791 ) ) ;
#4908=CONICAL_SURFACE ( 'NONE', #6817, 4.000000000000000000, 0.8911886515913786111 ) ;
#4914=CARTESIAN_POINT ( 'NONE',  ( 1.390230914382202032, 4.043987460488489560, -3.502507215260438844 ) ) ;
#4915=( NAMED_UNIT ( * ) PLANE_ANGLE_UNIT ( ) SI_UNIT ( $, .RADIAN. ) );
#4938=EDGE_LOOP ( 'NONE', ( #7193, #13086, #11703, #8686 ) ) ;
#4959=ORIENTED_EDGE ( 'NONE', *, *, #8001, .T. ) ;
#4963=CARTESIAN_POINT ( 'NONE',  ( -3.999999999999996447, -2.309401076758511806, -3.433295621305381573 ) ) ;
#4966=CARTESIAN_POINT ( 'NONE',  ( 4.207491450040565795, -2.029819825146484735, -3.671670828759566962 ) ) ;
#4984=FACE_OUTER_BOUND ( 'NONE', #8296, .T. ) ;
#4996=ORIENTED_EDGE ( 'NONE', *, *, #4187, .T. ) ;
#5001=LINE ( 'NONE', #13041, #2027 ) ;
#5002=VERTEX_POINT ( 'NONE', #21 ) ;
#5010=CARTESIAN_POINT ( 'NONE',  ( -0.1404048886732822965, -4.699864953788087441, -3.686887068327046268 ) ) ;
#5026=CARTESIAN_POINT ( 'NONE',  ( 0.3208286057739611619, -4.433571671609693787, -0.3503314178412661462 ) ) ;
#5028=ORIENTED_EDGE ( 'NONE', *, *, #11695, .T. ) ;
#5031=FACE_OUTER_BOUND ( 'NONE', #7936, .T. ) ;
#5046=EDGE_CURVE ( 'NONE', #13753, #13650, #9355, .T. ) ;
#5051=ORIENTED_EDGE ( 'NONE', *, *, #14652, .T. ) ;
#5054=CARTESIAN_POINT ( 'NONE',  ( -0.1410422978106116165, 4.700232962125094005, -3.687027686973625151 ) ) ;
#5071=EDGE_LOOP ( 'NONE', ( #1142, #12074 ) ) ;
#5077=STYLED_ITEM ( 'NONE', ( #12881 ), #1675 ) ;
#5089=CARTESIAN_POINT ( 'NONE',  ( -1.828356344711647763, -3.563200125723189338, -8.617289688891624500E-15 ) ) ;
#5108=AXIS2_PLACEMENT_3D ( 'NONE', #296, #6125, #10768 ) ;
#5113=CIRCLE ( 'NONE', #15, 4.000000000000000000 ) ;
#5142=ORIENTED_EDGE ( 'NONE', *, *, #9016, .F. ) ;
#5147=B_SPLINE_CURVE_WITH_KNOTS ( 'NONE', 3,
 ( #6057, #306, #3650, #8272, #5986, #8564 ),
 .UNSPECIFIED., .F., .F.,
 ( 4, 2, 4 ),
 ( 0.000000000000000000, 0.0002095117440864791795, 0.0004190234881729583589 ),
 .UNSPECIFIED. ) ;
#5150=CARTESIAN_POINT ( 'NONE',  ( 4.141042297810614059, -2.227970268150435640, -3.687027686973625151 ) ) ;
#5157=EDGE_CURVE ( 'NONE', #5547, #10917, #7699, .T. ) ;
#5167=CARTESIAN_POINT ( 'NONE',  ( -1.312671235360383548, -3.860931062424225235, -0.05923475698271134932 ) ) ;
#5173=ADVANCED_FACE ( 'NONE', ( #6157 ), #14145, .T. ) ;
#5191=DIRECTION ( 'NONE',  ( 0.000000000000000000, 0.000000000000000000, 1.000000000000000000 ) ) ;
#5193=EDGE_LOOP ( 'NONE', ( #7674, #1503, #1860, #3859 ) ) ;
#5198=CONICAL_SURFACE ( 'NONE', #7119, 2.500000000000000888, 0.9599310885968785900 ) ;
#5255=CARTESIAN_POINT ( 'NONE',  ( 0.000000000000000000, 0.000000000000000000, 0.000000000000000000 ) ) ;
#5256=CARTESIAN_POINT ( 'NONE',  ( 3.999999999999995559, 0.7924765000094657896, -0.05906175389889570942 ) ) ;
#5263=CARTESIAN_POINT ( 'NONE',  ( 0.000000000000000000, 4.618802153517009401, -3.433295621305381573 ) ) ;
#5265=ADVANCED_FACE ( 'NONE', ( #2831 ), #7444, .T. ) ;
#5270=CARTESIAN_POINT ( 'NONE',  ( -2.775557561562891351E-14, -4.618802153517009401, -0.5000000000000004441 ) ) ;
#5274=CARTESIAN_POINT ( 'NONE',  ( -4.235886605889385592, -2.417314728048545192, -3.751161874094021798 ) ) ;
#5293=FACE_OUTER_BOUND ( 'NONE', #771, .T. ) ;
#5297=ORIENTED_EDGE ( 'NONE', *, *, #5157, .T. ) ;
#5319=CARTESIAN_POINT ( 'NONE',  ( 4.211140560182194292, 2.431303136016534250, -3.745885042887433958 ) ) ;
#5322=VERTEX_POINT ( 'NONE', #3204 ) ;
#5341=CYLINDRICAL_SURFACE ( 'NONE', #3805, 2.100000000000000089 ) ;
#5350=ORIENTED_EDGE ( 'NONE', *, *, #2026, .T. ) ;
#5373=EDGE_CURVE ( 'NONE', #7535, #2855, #11880, .T. ) ;
#5404=ORIENTED_EDGE ( 'NONE', *, *, #3413, .T. ) ;
#5410=EDGE_LOOP ( 'NONE', ( #13270, #128, #5350, #14325 ) ) ;
#5413=CARTESIAN_POINT ( 'NONE',  ( -3.511755186886747371, 2.826662030176363860, -3.597382984111578974 ) ) ;
#5415=CARTESIAN_POINT ( 'NONE',  ( 2.000000000000000444, 3.464101615137758383, -3.142992957459237235 ) ) ;
#5433=ADVANCED_FACE ( 'NONE', ( #6681 ), #1320, .F. ) ;
#5448=VERTEX_POINT ( 'NONE', #5701 ) ;
#5498=CIRCLE ( 'NONE', #13493, 0.5155456020628804703 ) ;
#5502=B_SPLINE_CURVE_WITH_KNOTS ( 'NONE', 3,
 ( #4747, #9360, #7992, #12716, #1326, #5942, #12636, #13940 ),
 .UNSPECIFIED., .F., .F.,
 ( 4, 2, 2, 4 ),
 ( 2.465131517120937137E-07, 0.001183067374689842407, 0.001774477805458907686, 0.002365888236227972966 ),
 .UNSPECIFIED. ) ;
#5523=B_SPLINE_CURVE_WITH_KNOTS ( 'NONE', 3,
 ( #10275, #4518, #4886, #9417, #3747 ),
 .UNSPECIFIED., .F., .F.,
 ( 4, 1, 4 ),
 ( 0.000000000000000000, 0.002309401076758506657, 0.004618802153517013315 ),
 .UNSPECIFIED. ) ;
#5546=CARTESIAN_POINT ( 'NONE',  ( 0.000000000000000000, -4.862606272033110244, -3.745885042887441063 ) ) ;
#5547=VERTEX_POINT ( 'NONE', #8274 ) ;
#5572=DIRECTION ( 'NONE',  ( -0.8660254037844377084, -0.5000000000000015543, 0.000000000000000000 ) ) ;
#5587=AXIS2_PLACEMENT_3D ( 'NONE', #13765, #8276, #14055 ) ;
#5595=EDGE_CURVE ( 'NONE', #9910, #14881, #4801, .T. ) ;
#5617=DIRECTION ( 'NONE',  ( 0.000000000000000000, 0.000000000000000000, 1.000000000000000000 ) ) ;
#5621=CARTESIAN_POINT ( 'NONE',  ( -5.384454397937118664, 6.594054843588581554E-16, -4.484454397937119197 ) ) ;
#5622=EDGE_LOOP ( 'NONE', ( #3374, #2015, #8175, #319, #11691, #8953 ) ) ;
#5693=CARTESIAN_POINT ( 'NONE',  ( 3.999999999999996447, -2.309401076758518911, -0.5000000000000004441 ) ) ;
#5701=CARTESIAN_POINT ( 'NONE',  ( -5.384454397937118664, 6.702023979852546576E-16, -5.000000000000000888 ) ) ;
#5705=CARTESIAN_POINT ( 'NONE',  ( 2.344047193898588954, 3.265465875126466688, 1.943940613948618539E-16 ) ) ;
#5711=LINE ( 'NONE', #4798, #8523 ) ;
#5745=ORIENTED_EDGE ( 'NONE', *, *, #4408, .F. ) ;
#5752=ORIENTED_EDGE ( 'NONE', *, *, #12228, .F. ) ;
#5760=CARTESIAN_POINT ( 'NONE',  ( -1.257172072275683394, 3.892973519170756180, -3.433252694550406048 ) ) ;
#5794=MECHANICAL_DESIGN_GEOMETRIC_PRESENTATION_REPRESENTATION('',(#5077),#14545);
#5850=CARTESIAN_POINT ( 'NONE',  ( -3.999999999999998224, 0.8730739991738329930, -3.223134629628430226 ) ) ;
#5855=B_SPLINE_CURVE_WITH_KNOTS ( 'NONE', 3,
 ( #3055, #8808, #3197, #9028, #6676, #7671, #12315, #8726 ),
 .UNSPECIFIED., .F., .F.,
 ( 4, 2, 2, 4 ),
 ( 0.000000000000000000, 0.002450665683189820129, 0.003675998524784729327, 0.004901331366379639391 ),
 .UNSPECIFIED. ) ;
#5884=CARTESIAN_POINT ( 'NONE',  ( 4.175002511812153649, 2.208363329454889890, -3.469254087858246294 ) ) ;
#5894=CIRCLE ( 'NONE', #14146, 4.000000000000000000 ) ;
#5905=DIRECTION ( 'NONE',  ( 1.000000000000000000, 0.000000000000000000, 0.000000000000000000 ) ) ;
#5910=VECTOR ( 'NONE', #2445, 1000.000000000000000 ) ;
#5932=CARTESIAN_POINT ( 'NONE',  ( 0.000000000000000000, 4.618802153517009401, -0.5000000000000004441 ) ) ;
#5934=AXIS2_PLACEMENT_3D ( 'NONE', #5621, #3200, #14820 ) ;
#5942=CARTESIAN_POINT ( 'NONE',  ( -2.345747346278107770, 3.264484291692488771, -0.01223254789873306179 ) ) ;
#5943=CARTESIAN_POINT ( 'NONE',  ( -3.999999999999996447, 1.941961291383474952, -0.3515519931180187685 ) ) ;
#5944=MECHANICAL_DESIGN_GEOMETRIC_PRESENTATION_REPRESENTATION('',(#7888),#1601);
#5965=ADVANCED_FACE ( 'NONE', ( #9521 ), #10745, .F. ) ;
#5971=VERTEX_POINT ( 'NONE', #1564 ) ;
#5983=EDGE_CURVE ( 'NONE', #6726, #13811, #2064, .T. ) ;
#5984=CARTESIAN_POINT ( 'NONE',  ( -4.000000000000000000, -7.155734338404329264E-15, -3.142992957459235015 ) ) ;
#5986=CARTESIAN_POINT ( 'NONE',  ( -3.240162412667121864E-13, -4.796980096169331631, -3.721999068284310042 ) ) ;
#6006=ORIENTED_EDGE ( 'NONE', *, *, #2694, .F. ) ;
#6040=DIRECTION ( 'NONE',  ( 1.000000000000000000, 0.000000000000000000, 0.000000000000000000 ) ) ;
#6057=CARTESIAN_POINT ( 'NONE',  ( 0.000000000000000000, -4.618802153517023612, -3.433295621305388678 ) ) ;
#6109=ADVANCED_FACE ( 'NONE', ( #10053 ), #10200, .F. ) ;
#6125=DIRECTION ( 'NONE',  ( 0.000000000000000000, 0.000000000000000000, 1.000000000000000000 ) ) ;
#6129=ORIENTED_EDGE ( 'NONE', *, *, #12754, .T. ) ;
#6157=FACE_OUTER_BOUND ( 'NONE', #657, .T. ) ;
#6182=TOROIDAL_SURFACE ( 'NONE', #8132, 5.384454397937118664, 0.5155456020628804703 ) ;
#6184=CARTESIAN_POINT ( 'NONE',  ( -0.1756481739660510633, 4.720212674038980261, -3.469390959564067067 ) ) ;
#6190=AXIS2_PLACEMENT_3D ( 'NONE', #14957, #3487, #10389 ) ;
#6209=ORIENTED_EDGE ( 'NONE', *, *, #7070, .F. ) ;
#6220=DIRECTION ( 'NONE',  ( 0.000000000000000000, 0.000000000000000000, -1.000000000000000000 ) ) ;
#6229=DIRECTION ( 'NONE',  ( -1.000000000000000000, 0.000000000000000000, 0.000000000000000000 ) ) ;
#6242=EDGE_CURVE ( 'NONE', #13650, #12160, #5502, .T. ) ;
#6243=PLANE ( 'NONE',  #9476 ) ;
#6306=AXIS2_PLACEMENT_3D ( 'NONE', #7940, #11010, #2172 ) ;
#6309=CARTESIAN_POINT ( 'NONE',  ( 0.000000000000000000, 0.000000000000000000, -4.694516984716113228 ) ) ;
#6346=ORIENTED_EDGE ( 'NONE', *, *, #4329, .T. ) ;
#6375=ORIENTED_EDGE ( 'NONE', *, *, #9672, .T. ) ;
#6381=CIRCLE ( 'NONE', #14659, 2.500000000000000888 ) ;
#6387=DIRECTION ( 'NONE',  ( 1.000000000000000000, 0.000000000000000000, 0.000000000000000000 ) ) ;
#6390=CARTESIAN_POINT ( 'NONE',  ( 3.999999999999998224, 2.472263674411416812, -3.687027874309863229 ) ) ;
#6394=DIRECTION ( 'NONE',  ( -0.000000000000000000, -0.000000000000000000, 1.000000000000000000 ) ) ;
#6407=EDGE_LOOP ( 'NONE', ( #3224, #8332, #2273, #14174 ) ) ;
#6417=EDGE_CURVE ( 'NONE', #2568, #11548, #1933, .T. ) ;
#6423=ADVANCED_FACE ( 'NONE', ( #14450 ), #13574, .T. ) ;
#6425=COLOUR_RGB ( '', 0.66274510, 0.83137255, 0.94901961) ;
#6445=( BOUNDED_SURFACE ( )  B_SPLINE_SURFACE ( 3, 2, ( 
 ( #1658, #5010, #1510 ),
 ( #1432, #13126, #3797 ),
 ( #7421, #2867, #2641 ),
 ( #7257, #12137, #11999 ),
 ( #12067, #10913, #1587 ),
 ( #517, #5150, #10993 ) ),
 .UNSPECIFIED., .F., .F., .T. ) 
 B_SPLINE_SURFACE_WITH_KNOTS ( ( 4, 2, 4 ),
 ( 3, 3 ),
 ( 0.02032853247518126918, 0.02278863295364821906, 0.02524873343211517240 ),
 ( 0.000000000000000000, 1.000000000000000000 ),
 .UNSPECIFIED. ) 
 GEOMETRIC_REPRESENTATION_ITEM ( )  RATIONAL_B_SPLINE_SURFACE ( (
 ( 1.000000000000000000, 0.8047781615896836271, 1.000000000000000000),
 ( 1.000000000000000000, 0.8123767586289616371, 1.000000000000000000),
 ( 1.000000000000000000, 0.8190662415563912946, 1.000000000000000000),
 ( 1.000000000000000000, 0.8192361015669501478, 1.000000000000000000),
 ( 1.000000000000000000, 0.8126135807103542774, 1.000000000000000000),
 ( 1.000000000000000000, 0.8047712338318590009, 1.000000000000000000) ) ) 
 REPRESENTATION_ITEM ( '' )  SURFACE ( )  );
#6456=ORIENTED_EDGE ( 'NONE', *, *, #2694, .T. ) ;
#6469=CARTESIAN_POINT ( 'NONE',  ( 3.999999999999998224, -2.511475576507279595, -3.469253905236645341 ) ) ;
#6471=ADVANCED_FACE ( 'NONE', ( #7827 ), #14522, .F. ) ;
#6475=DIRECTION ( 'NONE',  ( 0.000000000000000000, 0.000000000000000000, -1.000000000000000000 ) ) ;
#6528=EDGE_CURVE ( 'NONE', #8812, #8852, #7559, .T. ) ;
#6533=( BOUNDED_SURFACE ( )  B_SPLINE_SURFACE ( 3, 2, ( 
 ( #9821, #14535, #5274 ),
 ( #8679, #12270, #4143 ),
 ( #13398, #1859, #10740 ),
 ( #8907, #3303, #4300 ),
 ( #7842, #11200, #6622 ),
 ( #13704, #2083, #14621 ) ),
 .UNSPECIFIED., .F., .F., .T. ) 
 B_SPLINE_SURFACE_WITH_KNOTS ( ( 4, 2, 4 ),
 ( 3, 3 ),
 ( 0.02032853247518126918, 0.02278863295364821906, 0.02524873343211516893 ),
 ( 0.000000000000000000, 1.000000000000000000 ),
 .UNSPECIFIED. ) 
 GEOMETRIC_REPRESENTATION_ITEM ( )  RATIONAL_B_SPLINE_SURFACE ( (
 ( 1.000000000000000000, 0.8047781615896838492, 1.000000000000000000),
 ( 1.000000000000000000, 0.8123767586290684406, 1.000000000000000000),
 ( 1.000000000000000000, 0.8190662415562490750, 1.000000000000000000),
 ( 1.000000000000000000, 0.8192361015670930335, 1.000000000000000000),
 ( 1.000000000000000000, 0.8126135807102463637, 1.000000000000000000),
 ( 1.000000000000000000, 0.8047712338318585568, 1.000000000000000000) ) ) 
 REPRESENTATION_ITEM ( '' )  SURFACE ( )  );
#6539=CARTESIAN_POINT ( 'NONE',  ( 3.999999999999999112, 0.8228435280417655262, -3.430609588141304123 ) ) ;
#6569=DIRECTION ( 'NONE',  ( 0.000000000000000000, 0.000000000000000000, 1.000000000000000000 ) ) ;
#6577=B_SPLINE_CURVE_WITH_KNOTS ( 'NONE', 3,
 ( #10136, #7472, #1798, #9988, #12348, #11063 ),
 .UNSPECIFIED., .F., .F.,
 ( 4, 2, 4 ),
 ( -3.640115492404583136E-06, 0.0002066546034003430006, 0.0004169493222930905534 ),
 .UNSPECIFIED. ) ;
#6599=EDGE_LOOP ( 'NONE', ( #13669, #14595, #2236 ) ) ;
#6607=EDGE_LOOP ( 'NONE', ( #12243, #13803, #912 ) ) ;
#6613=CARTESIAN_POINT ( 'NONE',  ( 0.000000000000000000, 4.862606272033088928, -3.745885042887437510 ) ) ;
#6614=VECTOR ( 'NONE', #8839, 1000.000000000000000 ) ;
#6622=CARTESIAN_POINT ( 'NONE',  ( -0.6810597143197720804, -4.461075778259609770, -3.598441714920719292 ) ) ;
#6649=DIRECTION ( 'NONE',  ( -0.000000000000000000, -0.000000000000000000, 1.000000000000000000 ) ) ;
#6656=VECTOR ( 'NONE', #6745, 999.9999999999998863 ) ;
#6658=AXIS2_PLACEMENT_3D ( 'NONE', #349, #9596, #9660 ) ;
#6676=CARTESIAN_POINT ( 'NONE',  ( 1.393927851585481159, -4.043713361053541178, -3.526374918436839145 ) ) ;
#6681=FACE_OUTER_BOUND ( 'NONE', #9838, .T. ) ;
#6690=CARTESIAN_POINT ( 'NONE',  ( 0.000000000000000000, -4.618802153517023612, -5.000000000000000888 ) ) ;
#6706=CARTESIAN_POINT ( 'NONE',  ( -0.6666666666666659635, 4.233901974057258322, -3.300726591567080703 ) ) ;
#6726=VERTEX_POINT ( 'NONE', #7279 ) ;
#6745=DIRECTION ( 'NONE',  ( 0.8191520442889875797, 0.000000000000000000, 0.5735764363510522656 ) ) ;
#6746=CARTESIAN_POINT ( 'NONE',  ( 3.999999999999997335, 1.941961291383485388, -0.3515519931180224322 ) ) ;
#6814=CARTESIAN_POINT ( 'NONE',  ( -0.3208286057739655472, 4.433571671609678688, -0.3503314178412536006 ) ) ;
#6817=AXIS2_PLACEMENT_3D ( 'NONE', #8835, #6475, #4448 ) ;
#6836=DIRECTION ( 'NONE',  ( 1.000000000000000000, 0.000000000000000000, 0.000000000000000000 ) ) ;
#6837=CARTESIAN_POINT ( 'NONE',  ( -4.203934362469272656, -1.640673743454848843, -3.598432614606966951 ) ) ;
#6864=CARTESIAN_POINT ( 'NONE',  ( -3.999999999999996447, -0.3979232138631226268, 2.786738396466647721E-15 ) ) ;
#6920=PLANE ( 'NONE',  #10341 ) ;
#6928=CARTESIAN_POINT ( 'NONE',  ( -3.999999999999995559, 0.7924765000094611267, -0.05906175389889475880 ) ) ;
#6931=ADVANCED_FACE ( 'NONE', ( #14430, #8645 ), #9082, .T. ) ;
#6962=CARTESIAN_POINT ( 'NONE',  ( -1.317756351988341290, 3.857995168970199895, -0.04852650426601234218 ) ) ;
#6963=CARTESIAN_POINT ( 'NONE',  ( -3.522875095019435854, 2.820352903225096686, -3.598441714920458612 ) ) ;
#6972=ORIENTED_EDGE ( 'NONE', *, *, #3939, .F. ) ;
#6993=CARTESIAN_POINT ( 'NONE',  ( -3.999999999999996447, 2.309401076758498039, -0.4999999999999935052 ) ) ;
#7011=CARTESIAN_POINT ( 'NONE',  ( 2.756197834950067538, 3.027510591568720599, -3.223146290109807133 ) ) ;
#7033=CARTESIAN_POINT ( 'NONE',  ( -0.6640947660594231916, 4.471078309994339861, -3.602146406945769819 ) ) ;
#7050=FACE_OUTER_BOUND ( 'NONE', #5193, .T. ) ;
#7051=AXIS2_PLACEMENT_3D ( 'NONE', #12596, #2047, #2193 ) ;
#7059=EDGE_LOOP ( 'NONE', ( #5028, #6006, #9066 ) ) ;
#7061=CARTESIAN_POINT ( 'NONE',  ( -2.000000000000008882, -3.464101615137750390, 0.000000000000000000 ) ) ;
#7070=EDGE_CURVE ( 'NONE', #1683, #3137, #2554, .T. ) ;
#7119=AXIS2_PLACEMENT_3D ( 'NONE', #14988, #13774, #8290 ) ;
#7120=VECTOR ( 'NONE', #6569, 1000.000000000000000 ) ;
#7122=SURFACE_STYLE_USAGE ( .BOTH. , #4864 ) ;
#7134=CARTESIAN_POINT ( 'NONE',  ( -4.197312064133470244, -0.8182229787989945269, -3.502518405183887573 ) ) ;
#7140=CARTESIAN_POINT ( 'NONE',  ( 1.144235203016665592, 3.958177651039090250, -0.09382832055445507191 ) ) ;
#7158=VERTEX_POINT ( 'NONE', #12194 ) ;
#7171=( NAMED_UNIT ( * ) SI_UNIT ( $, .STERADIAN. ) SOLID_ANGLE_UNIT ( ) );
#7175=EDGE_LOOP ( 'NONE', ( #12366, #12078, #14767, #14493, #8269, #12749, #183 ) ) ;
#7188=CARTESIAN_POINT ( 'NONE',  ( -3.999999999999996447, -2.309401076758512250, -3.504269196027871569 ) ) ;
#7193=ORIENTED_EDGE ( 'NONE', *, *, #2763, .T. ) ;
#7197=PRESENTATION_STYLE_ASSIGNMENT (( #7122 ) ) ;
#7218=CARTESIAN_POINT ( 'NONE',  ( -3.333333333333330373, -2.694301256218263330, -3.300726591567081147 ) ) ;
#7223=DIRECTION ( 'NONE',  ( 0.000000000000000000, 0.000000000000000000, -1.000000000000000000 ) ) ;
#7257=CARTESIAN_POINT ( 'NONE',  ( 2.725741868436124538, -3.045094352033993701, -3.220599429844053674 ) ) ;
#7273=CARTESIAN_POINT ( 'NONE',  ( 3.999999999999996447, -0.7890432684750899872, -0.04868663549882019242 ) ) ;
#7279=CARTESIAN_POINT ( 'NONE',  ( -5.560781378645575757, 6.809993116116508640E-16, -4.000000000000000000 ) ) ;
#7310=B_SPLINE_CURVE_WITH_KNOTS ( 'NONE', 3,
 ( #12544, #4502, #2132, #13593 ),
 .UNSPECIFIED., .F., .F.,
 ( 4, 4 ),
 ( 0.000000000000000000, 0.002452478801916377609 ),
 .UNSPECIFIED. ) ;
#7323=EDGE_LOOP ( 'NONE', ( #14696, #10759, #6129, #2994 ) ) ;
#7330=CARTESIAN_POINT ( 'NONE',  ( 0.000000000000000000, 0.000000000000000000, 0.000000000000000000 ) ) ;
#7359=CARTESIAN_POINT ( 'NONE',  ( -0.3198814748697815791, -4.434118497892180599, -0.3507732604232504658 ) ) ;
#7402=CARTESIAN_POINT ( 'NONE',  ( 3.333333333333338810, -2.694301256218270435, -3.300726591567082480 ) ) ;
#7411=CIRCLE ( 'NONE', #9104, 2.500000000000000444 ) ;
#7421=CARTESIAN_POINT ( 'NONE',  ( 1.243802165048770725, -3.900692638707479620, -3.223146290109812462 ) ) ;
#7436=VERTEX_POINT ( 'NONE', #1252 ) ;
#7444=PLANE ( 'NONE',  #9304 ) ;
#7453=ADVANCED_FACE ( 'NONE', ( #1112 ), #986, .F. ) ;
#7462=CARTESIAN_POINT ( 'NONE',  ( 3.999999999999996447, 2.309401076758498039, -5.000000000000000888 ) ) ;
#7463=ORIENTED_EDGE ( 'NONE', *, *, #10741, .F. ) ;
#7472=CARTESIAN_POINT ( 'NONE',  ( -3.941339353050220809E-13, 4.796734841935198723, -3.721909803043260467 ) ) ;
#7483=CARTESIAN_POINT ( 'NONE',  ( -4.211140560182194292, -2.431303136016555122, -3.745885042887437510 ) ) ;
#7491=ORIENTED_EDGE ( 'NONE', *, *, #9672, .F. ) ;
#7528=VECTOR ( 'NONE', #2623, 999.9999999999998863 ) ;
#7535=VERTEX_POINT ( 'NONE', #10730 ) ;
#7539=ORIENTED_EDGE ( 'NONE', *, *, #8699, .T. ) ;
#7552=CARTESIAN_POINT ( 'NONE',  ( -4.197393957002300446, -7.680494662014190109E-14, -3.503767560748928922 ) ) ;
#7559=B_SPLINE_CURVE_WITH_KNOTS ( 'NONE', 3,
 ( #1909, #5413, #3131, #8962, #10112, #14754, #13602, #13991 ),
 .UNSPECIFIED., .F., .F.,
 ( 4, 2, 2, 4 ),
 ( 0.000000000000000000, 0.002450665683189819696, 0.003675998524784731061, 0.004901331366379641993 ),
 .UNSPECIFIED. ) ;
#7571=CARTESIAN_POINT ( 'NONE',  ( 2.687328764639642653, -3.067272167851296860, -0.05923475698271275791 ) ) ;
#7574=EDGE_LOOP ( 'NONE', ( #7463, #12648, #3870, #8109, #12248 ) ) ;
#7587=ORIENTED_EDGE ( 'NONE', *, *, #1380, .F. ) ;
#7589=FACE_OUTER_BOUND ( 'NONE', #7175, .T. ) ;
#7599=CARTESIAN_POINT ( 'NONE',  ( -2.100000000000000089, 2.571758278209443929E-16, -4.694516984716113228 ) ) ;
#7606=AXIS2_PLACEMENT_3D ( 'NONE', #8585, #11801, #13010 ) ;
#7615=CARTESIAN_POINT ( 'NONE',  ( 3.999999999999998224, 1.658577278524641763, -3.531553309554042119 ) ) ;
#7617=CONICAL_SURFACE ( 'NONE', #4004, 4.000000000000000000, 0.8911886515913786111 ) ;
#7622=FACE_OUTER_BOUND ( 'NONE', #6607, .T. ) ;
#7671=CARTESIAN_POINT ( 'NONE',  ( 0.6937372685066667266, -4.453844082567734119, -3.610536846335893113 ) ) ;
#7674=ORIENTED_EDGE ( 'NONE', *, *, #4218, .F. ) ;
#7680=EDGE_LOOP ( 'NONE', ( #75, #9677, #9135 ) ) ;
#7699=B_SPLINE_CURVE_WITH_KNOTS ( 'NONE', 3,
 ( #4963, #7218, #12930, #14364, #3971 ),
 .UNSPECIFIED., .F., .F.,
 ( 4, 1, 4 ),
 ( 0.000000000000000000, 0.002309401076758505790, 0.004618802153517011580 ),
 .UNSPECIFIED. ) ;
#7719=CARTESIAN_POINT ( 'NONE',  ( 3.999999999999996447, -2.309401076758518911, -0.5000000000000004441 ) ) ;
#7738=CARTESIAN_POINT ( 'NONE',  ( -2.449848172108558764, -3.432307619358751172, -3.503702292528908302 ) ) ;
#7740=CARTESIAN_POINT ( 'NONE',  ( 2.100000000000000089, 0.000000000000000000, -0.2800830152838856835 ) ) ;
#7742=DIRECTION ( 'NONE',  ( -0.8660254037844373753, 0.5000000000000021094, 0.000000000000000000 ) ) ;
#7759=DIRECTION ( 'NONE',  ( 0.000000000000000000, 0.000000000000000000, 1.000000000000000000 ) ) ;
#7793=FACE_OUTER_BOUND ( 'NONE', #7680, .T. ) ;
#7814=EDGE_CURVE ( 'NONE', #5448, #14675, #1199, .T. ) ;
#7827=FACE_OUTER_BOUND ( 'NONE', #6407, .T. ) ;
#7828=CARTESIAN_POINT ( 'NONE',  ( 3.333333333333331261, 2.694301256218251339, -3.300726591567078483 ) ) ;
#7835=FACE_OUTER_BOUND ( 'NONE', #5622, .T. ) ;
#7842=CARTESIAN_POINT ( 'NONE',  ( -0.5449313310646759501, -4.304185902836972666, -3.316620875263518453 ) ) ;
#7852=CIRCLE ( 'NONE', #11996, 4.000000000000000000 ) ;
#7859=ADVANCED_FACE ( 'NONE', ( #1229 ), #14724, .F. ) ;
#7874=CARTESIAN_POINT ( 'NONE',  ( 4.211140560182194292, -2.431303136016555122, -3.745885042887437510 ) ) ;
#7875=ORIENTED_EDGE ( 'NONE', *, *, #11512, .F. ) ;
#7880=ORIENTED_EDGE ( 'NONE', *, *, #1250, .F. ) ;
#7888=STYLED_ITEM ( 'NONE', ( #7197 ), #4390 ) ;
#7900=LINE ( 'NONE', #14899, #6656 ) ;
#7903=CARTESIAN_POINT ( 'NONE',  ( 3.999999999999996447, 2.309401076758498039, -3.433295621305378020 ) ) ;
#7908=CONICAL_SURFACE ( 'NONE', #2569, 4.000000000000000000, 0.8911886515913786111 ) ;
#7911=LINE ( 'NONE', #6690, #294 ) ;
#7936=EDGE_LOOP ( 'NONE', ( #2358, #2227, #14084, #5404, #1662 ) ) ;
#7940=CARTESIAN_POINT ( 'NONE',  ( 0.000000000000000000, 4.618802153517009401, -5.000000000000000888 ) ) ;
#7942=LINE ( 'NONE', #10000, #3320 ) ;
#7957=CARTESIAN_POINT ( 'NONE',  ( -2.807080416178826088, 3.225969019225362722, -3.502507215260544982 ) ) ;
#7963=EDGE_LOOP ( 'NONE', ( #7539, #14256, #7880, #13740, #6972 ) ) ;
#7965=CARTESIAN_POINT ( 'NONE',  ( -4.207491450040565795, 2.029819825146467416, -3.671670828759564742 ) ) ;
#7972=CARTESIAN_POINT ( 'NONE',  ( 3.510273485745305955, 2.827716139362653092, -3.610536846335885564 ) ) ;
#7976=CARTESIAN_POINT ( 'NONE',  ( -3.999999999999634959, -1.658469974638516753, -3.531532913076921076 ) ) ;
#7992=CARTESIAN_POINT ( 'NONE',  ( -3.355112389629167691, 2.681727112203151631, -0.2256878752776672603 ) ) ;
#8001=EDGE_CURVE ( 'NONE', #2326, #7158, #2327, .T. ) ;
#8054=ORIENTED_EDGE ( 'NONE', *, *, #3102, .T. ) ;
#8065=CIRCLE ( 'NONE', #10731, 5.384454397937118664 ) ;
#8074=AXIS2_PLACEMENT_3D ( 'NONE', #12026, #9638, #1537 ) ;
#8109=ORIENTED_EDGE ( 'NONE', *, *, #6242, .T. ) ;
#8112=CARTESIAN_POINT ( 'NONE',  ( -3.999999999999996447, 2.309401076758498039, -3.433295621305378020 ) ) ;
#8114=CARTESIAN_POINT ( 'NONE',  ( -4.141042297810613171, 2.227970268150412991, -3.687027686973620266 ) ) ;
#8132=AXIS2_PLACEMENT_3D ( 'NONE', #4847, #13750, #3339 ) ;
#8133=CARTESIAN_POINT ( 'NONE',  ( -5.560781378645573980, 0.000000000000000000, -4.000000000000000000 ) ) ;
#8175=ORIENTED_EDGE ( 'NONE', *, *, #4618, .F. ) ;
#8198=ADVANCED_FACE ( 'NONE', ( #995 ), #475, .T. ) ;
#8206=CARTESIAN_POINT ( 'NONE',  ( -3.999999999999998224, 1.700094919196804666, -3.320312364301445385 ) ) ;
#8223=ORIENTED_EDGE ( 'NONE', *, *, #3939, .T. ) ;
#8224=ORIENTED_EDGE ( 'NONE', *, *, #4187, .F. ) ;
#8227=DIRECTION ( 'NONE',  ( 0.000000000000000000, 0.000000000000000000, -1.000000000000000000 ) ) ;
#8269=ORIENTED_EDGE ( 'NONE', *, *, #1380, .T. ) ;
#8272=CARTESIAN_POINT ( 'NONE',  ( 2.278234631210864708E-15, -4.736529461166055555, -3.681130640444385094 ) ) ;
#8274=CARTESIAN_POINT ( 'NONE',  ( -3.999999999999996447, -2.309401076758511806, -3.433295621305381573 ) ) ;
#8276=DIRECTION ( 'NONE',  ( -0.000000000000000000, -0.000000000000000000, 1.000000000000000000 ) ) ;
#8281=CARTESIAN_POINT ( 'NONE',  ( -4.204114297095385311, 1.660363174096626260, -3.602136431857864807 ) ) ;
#8290=DIRECTION ( 'NONE',  ( -1.000000000000000000, 0.000000000000000000, 0.000000000000000000 ) ) ;
#8296=EDGE_LOOP ( 'NONE', ( #13550, #11767, #445, #6375, #5051 ) ) ;
#8312=ORIENTED_EDGE ( 'NONE', *, *, #4329, .F. ) ;
#8332=ORIENTED_EDGE ( 'NONE', *, *, #2945, .T. ) ;
#8339=CARTESIAN_POINT ( 'NONE',  ( 0.000000000000000000, 0.000000000000000000, 0.000000000000000000 ) ) ;
#8352=CARTESIAN_POINT ( 'NONE',  ( 3.999999999999995559, -1.942223658245636253, -0.3516579909967626483 ) ) ;
#8400=AXIS2_PLACEMENT_3D ( 'NONE', #3122, #6220, #10940 ) ;
#8447=DIRECTION ( 'NONE',  ( 1.000000000000000000, 0.000000000000000000, 0.000000000000000000 ) ) ;
#8523=VECTOR ( 'NONE', #9194, 1000.000000000000114 ) ;
#8533=EDGE_LOOP ( 'NONE', ( #5142, #10683, #2356, #13427 ) ) ;
#8536=CARTESIAN_POINT ( 'NONE',  ( 3.999999999999996447, 2.309401076758498039, -5.000000000000000888 ) ) ;
#8564=CARTESIAN_POINT ( 'NONE',  ( 0.000000000000000000, -4.862606272033110244, -3.745885042887441063 ) ) ;
#8581=EDGE_LOOP ( 'NONE', ( #9840, #2917, #11066, #7587, #8224 ) ) ;
#8585=CARTESIAN_POINT ( 'NONE',  ( -3.999999999999996447, -2.309401076758511806, -5.000000000000000888 ) ) ;
#8609=DIRECTION ( 'NONE',  ( 0.000000000000000000, 0.000000000000000000, 1.000000000000000000 ) ) ;
#8623=CARTESIAN_POINT ( 'NONE',  ( -3.999999999999996447, -2.309401076758518911, -0.5000000000000004441 ) ) ;
#8631=FACE_OUTER_BOUND ( 'NONE', #14308, .T. ) ;
#8645=FACE_OUTER_BOUND ( 'NONE', #5071, .T. ) ;
#8648=ORIENTED_EDGE ( 'NONE', *, *, #10614, .T. ) ;
#8657=EDGE_LOOP ( 'NONE', ( #11974, #10212 ) ) ;
#8679=CARTESIAN_POINT ( 'NONE',  ( -3.472371940586000072, -2.614027278893185979, -3.320322319202478223 ) ) ;
#8686=ORIENTED_EDGE ( 'NONE', *, *, #4264, .F. ) ;
#8698=CARTESIAN_POINT ( 'NONE',  ( 0.000000000000000000, -4.862606272033110244, -3.745885042887441063 ) ) ;
#8699=EDGE_CURVE ( 'NONE', #10230, #11793, #12770, .T. ) ;
#8726=CARTESIAN_POINT ( 'NONE',  ( 0.000000000000000000, -4.862606272033110244, -3.745885042887441063 ) ) ;
#8744=CARTESIAN_POINT ( 'NONE',  ( 0.000000000000000000, 0.000000000000000000, -4.974599999999998801 ) ) ;
#8754=CARTESIAN_POINT ( 'NONE',  ( 3.999999999999998224, 1.680228229147135544, -3.316631783032547354 ) ) ;
#8776=ORIENTED_EDGE ( 'NONE', *, *, #4264, .T. ) ;
#8799=UNCERTAINTY_MEASURE_WITH_UNIT (LENGTH_MEASURE( 1.000000000000000082E-05 ), #10701, 'distance_accuracy_value', 'NONE');
#8808=CARTESIAN_POINT ( 'NONE',  ( 3.511755186886751368, -2.826662030176382068, -3.597382984111583415 ) ) ;
#8812=VERTEX_POINT ( 'NONE', #12261 ) ;
#8817=CARTESIAN_POINT ( 'NONE',  ( 0.000000000000000000, 0.000000000000000000, -5.000000000000000888 ) ) ;
#8827=DIRECTION ( 'NONE',  ( -1.000000000000000000, 0.000000000000000000, 0.000000000000000000 ) ) ;
#8835=CARTESIAN_POINT ( 'NONE',  ( 0.000000000000000000, 0.000000000000000000, 0.000000000000000000 ) ) ;
#8839=DIRECTION ( 'NONE',  ( 0.000000000000000000, 0.000000000000000000, 1.000000000000000000 ) ) ;
#8852=VERTEX_POINT ( 'NONE', #6613 ) ;
#8898=EDGE_CURVE ( 'NONE', #10917, #2326, #7911, .T. ) ;
#8907=CARTESIAN_POINT ( 'NONE',  ( -1.274258131565023877, -3.883108878240887130, -3.220599429844052342 ) ) ;
#8932=CARTESIAN_POINT ( 'NONE',  ( 3.680118525130242180, -2.494084732383343272, -0.3507732604232501328 ) ) ;
#8948=COLOUR_RGB ( '', 0.66274510, 0.83137255, 0.94901961) ;
#8952=CARTESIAN_POINT ( 'NONE',  ( -2.804994570502170603, -3.229033611042463114, -3.526374918436837813 ) ) ;
#8953=ORIENTED_EDGE ( 'NONE', *, *, #11695, .F. ) ;
#8962=CARTESIAN_POINT ( 'NONE',  ( -1.747541505913279947, 3.837784562140252653, -3.503702292528905637 ) ) ;
#9016=EDGE_CURVE ( 'NONE', #2530, #2568, #5711, .T. ) ;
#9022=CARTESIAN_POINT ( 'NONE',  ( 0.1404048886732826851, 4.699864953788067901, -3.686887068327037831 ) ) ;
#9028=CARTESIAN_POINT ( 'NONE',  ( 1.747541505913281279, -3.837784562140267308, -3.503702292528909190 ) ) ;
#9043=CARTESIAN_POINT ( 'NONE',  ( 2.500000000000000444, 0.000000000000000000, -5.000000000000000888 ) ) ;
#9047=CARTESIAN_POINT ( 'NONE',  ( 5.384454397937118664, 0.000000000000000000, -4.484454397937119197 ) ) ;
#9058=DIRECTION ( 'NONE',  ( 1.000000000000000000, 0.000000000000000000, 0.000000000000000000 ) ) ;
#9066=ORIENTED_EDGE ( 'NONE', *, *, #11523, .F. ) ;
#9071=( BOUNDED_SURFACE ( )  B_SPLINE_SURFACE ( 3, 2, ( 
 ( #6469, #4137, #566 ),
 ( #11272, #876, #13471 ),
 ( #2992, #13392, #13314 ),
 ( #11119, #6539, #4362 ),
 ( #8754, #7615, #11197 ),
 ( #13613, #6390, #1701 ) ),
 .UNSPECIFIED., .F., .F., .T. ) 
 B_SPLINE_SURFACE_WITH_KNOTS ( ( 4, 2, 4 ),
 ( 3, 3 ),
 ( 0.02027065861071770947, 0.02273072267836921331, 0.02519078674602071716 ),
 ( 0.000000000000000000, 1.000000000000000000 ),
 .UNSPECIFIED. ) 
 GEOMETRIC_REPRESENTATION_ITEM ( )  RATIONAL_B_SPLINE_SURFACE ( (
 ( 1.000000000000000000, 0.8047781708337298223, 1.000000000000000000),
 ( 1.000000000000000000, 0.8123765190704248518, 1.000000000000000000),
 ( 1.000000000000000000, 0.8190656277165397903, 1.000000000000000000),
 ( 1.000000000000000000, 0.8192366903510730491, 1.000000000000000000),
 ( 1.000000000000000000, 0.8126138454303968306, 1.000000000000000000),
 ( 1.000000000000000000, 0.8047712246031420991, 1.000000000000000000) ) ) 
 REPRESENTATION_ITEM ( '' )  SURFACE ( )  );
#9072=CARTESIAN_POINT ( 'NONE',  ( -3.999999999999996447, -2.309401076758518911, -0.5000000000000004441 ) ) ;
#9082=PLANE ( 'NONE',  #6306 ) ;
#9095=EDGE_LOOP ( 'NONE', ( #11862, #12019, #12337, #4642 ) ) ;
#9104=AXIS2_PLACEMENT_3D ( 'NONE', #3335, #2117, #12528 ) ;
#9135=ORIENTED_EDGE ( 'NONE', *, *, #6242, .F. ) ;
#9142=CARTESIAN_POINT ( 'NONE',  ( 0.000000000000000000, 4.618802153517009401, -3.433295621305381573 ) ) ;
#9143=ORIENTED_EDGE ( 'NONE', *, *, #13225, .T. ) ;
#9176=CARTESIAN_POINT ( 'NONE',  ( 0.1750025118121574796, 4.719839900820618439, -3.469254087858248514 ) ) ;
#9186=DIRECTION ( 'NONE',  ( -1.000000000000000000, 0.000000000000000000, 0.000000000000000000 ) ) ;
#9194=DIRECTION ( 'NONE',  ( 0.8191520442889902442, 1.003171929053522651E-16, -0.5735764363510482688 ) ) ;
#9232=CARTESIAN_POINT ( 'NONE',  ( -2.059999999999998721, 2.522772406243545965E-16, -0.3080913168122742518 ) ) ;
#9266=EDGE_CURVE ( 'NONE', #7158, #5002, #5113, .T. ) ;
#9288=CARTESIAN_POINT ( 'NONE',  ( -3.999999999999996447, 2.309401076758498039, -3.433295621305378020 ) ) ;
#9301=CARTESIAN_POINT ( 'NONE',  ( 4.140404888673279160, 2.228338276487440428, -3.686887068327035610 ) ) ;
#9303=CARTESIAN_POINT ( 'NONE',  ( -2.100000000000000089, 2.571758278209443929E-16, -0.2800830152838856835 ) ) ;
#9304=AXIS2_PLACEMENT_3D ( 'NONE', #12093, #4807, #7742 ) ;
#9338=CARTESIAN_POINT ( 'NONE',  ( 1.391697335622809728, 4.043246145443373685, -3.503898532754365913 ) ) ;
#9344=CARTESIAN_POINT ( 'NONE',  ( -4.211399284164270007, 2.459729995988209073, -3.751162237960540491 ) ) ;
#9355=LINE ( 'NONE', #1027, #5910 ) ;
#9360=CARTESIAN_POINT ( 'NONE',  ( -3.680118525130241736, 2.494084732383326841, -0.3507732604232432494 ) ) ;
#9376=CARTESIAN_POINT ( 'NONE',  ( 1.274258131565028318, 3.883108878240871586, -3.220599429844048789 ) ) ;
#9380=ORIENTED_EDGE ( 'NONE', *, *, #6528, .F. ) ;
#9388=VERTEX_POINT ( 'NONE', #71 ) ;
#9409=CARTESIAN_POINT ( 'NONE',  ( 5.384454397937118664, 0.000000000000000000, -5.000000000000000888 ) ) ;
#9415=CARTESIAN_POINT ( 'NONE',  ( 1.654252653721904442, 3.663718938583012896, -0.01223254789873389446 ) ) ;
#9416=CARTESIAN_POINT ( 'NONE',  ( -3.999999999999996447, -2.309401076758518911, -0.5000000000000004441 ) ) ;
#9417=CARTESIAN_POINT ( 'NONE',  ( 3.999999999999998224, 1.539600717838995658, -3.300726591567077151 ) ) ;
#9425=EDGE_CURVE ( 'NONE', #13753, #5547, #3133, .T. ) ;
#9428=DIRECTION ( 'NONE',  ( 1.000000000000000000, 0.000000000000000000, 0.000000000000000000 ) ) ;
#9446=CARTESIAN_POINT ( 'NONE',  ( 3.999999999999996447, -2.309401076758518911, -3.433295621305385126 ) ) ;
#9457=ORIENTED_EDGE ( 'NONE', *, *, #1273, .F. ) ;
#9476=AXIS2_PLACEMENT_3D ( 'NONE', #12110, #3917, #2996 ) ;
#9521=FACE_OUTER_BOUND ( 'NONE', #11068, .T. ) ;
#9540=B_SPLINE_CURVE_WITH_KNOTS ( 'NONE', 3,
 ( #7061, #93, #11504, #4738, #3593, #9416 ),
 .UNSPECIFIED., .F., .F.,
 ( 4, 2, 4 ),
 ( 0.002365888236228000721, 0.003551327329835088017, 0.004736766423442175314 ),
 .UNSPECIFIED. ) ;
#9588=EDGE_CURVE ( 'NONE', #9923, #11548, #4096, .T. ) ;
#9596=DIRECTION ( 'NONE',  ( -0.000000000000000000, -0.000000000000000000, 1.000000000000000000 ) ) ;
#9603=ORIENTED_EDGE ( 'NONE', *, *, #8898, .T. ) ;
#9638=DIRECTION ( 'NONE',  ( -1.000000000000000000, 0.000000000000000000, 0.000000000000000000 ) ) ;
#9642=CARTESIAN_POINT ( 'NONE',  ( 4.211140560182194292, -2.431303136016555122, -3.745885042887437510 ) ) ;
#9660=DIRECTION ( 'NONE',  ( 1.000000000000000000, 0.000000000000000000, 0.000000000000000000 ) ) ;
#9672=EDGE_CURVE ( 'NONE', #2995, #5322, #2790, .T. ) ;
#9677=ORIENTED_EDGE ( 'NONE', *, *, #13577, .T. ) ;
#9700=EDGE_CURVE ( 'NONE', #9830, #11793, #2058, .T. ) ;
#9703=CARTESIAN_POINT ( 'NONE',  ( 2.000000000000008882, -3.464101615137750390, 0.000000000000000000 ) ) ;
#9708=EDGE_CURVE ( 'NONE', #12909, #10622, #1934, .T. ) ;
#9809=ORIENTED_EDGE ( 'NONE', *, *, #14721, .T. ) ;
#9821=CARTESIAN_POINT ( 'NONE',  ( -4.175002511812149208, -2.208363329454906765, -3.469254087858247626 ) ) ;
#9830=VERTEX_POINT ( 'NONE', #11954 ) ;
#9838=EDGE_LOOP ( 'NONE', ( #2786, #14540, #3591, #10725 ) ) ;
#9840=ORIENTED_EDGE ( 'NONE', *, *, #11705, .T. ) ;
#9850=CARTESIAN_POINT ( 'NONE',  ( 2.000000000000008882, -3.464101615137750390, 0.000000000000000000 ) ) ;
#9867=CARTESIAN_POINT ( 'NONE',  ( -0.6920835326022556355, -4.454600218803903999, -3.597382984111584747 ) ) ;
#9881=DIRECTION ( 'NONE',  ( 1.000000000000000000, 0.000000000000000000, 0.000000000000000000 ) ) ;
#9884=ORIENTED_EDGE ( 'NONE', *, *, #1518, .T. ) ;
#9898=LINE ( 'NONE', #12419, #6614 ) ;
#9910=VERTEX_POINT ( 'NONE', #7903 ) ;
#9923=VERTEX_POINT ( 'NONE', #7599 ) ;
#9935=CARTESIAN_POINT ( 'NONE',  ( -2.712762565639317280, 3.052587955997805302, -3.430618716626997688 ) ) ;
#9965=DIRECTION ( 'NONE',  ( 0.000000000000000000, 0.000000000000000000, 1.000000000000000000 ) ) ;
#9988=CARTESIAN_POINT ( 'NONE',  ( 5.196599455413437438E-15, 4.647089433458989838, -3.572167766733754135 ) ) ;
#9995=ORIENTED_EDGE ( 'NONE', *, *, #4589, .T. ) ;
#10000=CARTESIAN_POINT ( 'NONE',  ( -2.500000000000000444, 3.061616997868383634E-16, -25.03750572909317285 ) ) ;
#10006=ADVANCED_FACE ( 'NONE', ( #7050 ), #12144, .T. ) ;
#10022=EDGE_CURVE ( 'NONE', #8852, #14881, #13614, .T. ) ;
#10053=FACE_OUTER_BOUND ( 'NONE', #3677, .T. ) ;
#10112=CARTESIAN_POINT ( 'NONE',  ( -1.393927851585479605, 4.043713361053526079, -3.526374918436835149 ) ) ;
#10136=CARTESIAN_POINT ( 'NONE',  ( 0.000000000000000000, 4.862606272033088928, -3.745885042887437510 ) ) ;
#10177=AXIS2_PLACEMENT_3D ( 'NONE', #1621, #4052, #14519 ) ;
#10199=ORIENTED_EDGE ( 'NONE', *, *, #12185, .F. ) ;
#10200=CYLINDRICAL_SURFACE ( 'NONE', #3281, 2.500000000000000444 ) ;
#10212=ORIENTED_EDGE ( 'NONE', *, *, #14090, .F. ) ;
#10230=VERTEX_POINT ( 'NONE', #227 ) ;
#10248=CARTESIAN_POINT ( 'NONE',  ( -0.5276280594147905179, 4.314175951381877816, -3.320322319202512418 ) ) ;
#10259=CIRCLE ( 'NONE', #13415, 4.000000000000000000 ) ;
#10267=DIRECTION ( 'NONE',  ( -0.000000000000000000, -0.000000000000000000, 1.000000000000000000 ) ) ;
#10275=CARTESIAN_POINT ( 'NONE',  ( 3.999999999999996447, -2.309401076758518911, -3.433295621305385126 ) ) ;
#10323=DIRECTION ( 'NONE',  ( 0.9396926207859138680, 1.150791560227856926E-16, -0.3420201433256536139 ) ) ;
#10331=CARTESIAN_POINT ( 'NONE',  ( -4.198928548860770604, 0.8158838809860071706, -3.526471437616916837 ) ) ;
#10336=CARTESIAN_POINT ( 'NONE',  ( 3.999999999999996447, 2.309401076758511806, -0.5000000000000004441 ) ) ;
#10341=AXIS2_PLACEMENT_3D ( 'NONE', #1169, #2228, #945 ) ;
#10342=CARTESIAN_POINT ( 'NONE',  ( -4.211405944401396262, -2.460460786169389014, -3.751298493805494960 ) ) ;
#10349=FACE_OUTER_BOUND ( 'NONE', #8533, .T. ) ;
#10371=EDGE_LOOP ( 'NONE', ( #13790, #10904, #5745, #13778 ) ) ;
#10380=CARTESIAN_POINT ( 'NONE',  ( 4.000000000000000000, -2.309401076758517135, -3.504271511727127475 ) ) ;
#10389=DIRECTION ( 'NONE',  ( -1.000000000000000000, 0.000000000000000000, 0.000000000000000000 ) ) ;
#10394=CARTESIAN_POINT ( 'NONE',  ( -1.655952806101423258, 3.662737355149033203, 1.383628319339899209E-15 ) ) ;
#10397=DIRECTION ( 'NONE',  ( -1.000000000000000000, 0.000000000000000000, 0.000000000000000000 ) ) ;
#10414=DIRECTION ( 'NONE',  ( 0.000000000000000000, 0.000000000000000000, -1.000000000000000000 ) ) ;
#10434=DIRECTION ( 'NONE',  ( 0.000000000000000000, 0.000000000000000000, -1.000000000000000000 ) ) ;
#10455=CARTESIAN_POINT ( 'NONE',  ( 4.211140560182194292, 2.431303136016534250, -3.745885042887433958 ) ) ;
#10466=CARTESIAN_POINT ( 'NONE',  ( -3.999999999999996447, 2.309401076758498039, -0.4999999999999935052 ) ) ;
#10487=CARTESIAN_POINT ( 'NONE',  ( 0.000000000000000000, 0.000000000000000000, -5.000000000000000888 ) ) ;
#10508=ORIENTED_EDGE ( 'NONE', *, *, #4552, .T. ) ;
#10530=CARTESIAN_POINT ( 'NONE',  ( 4.101954839143203024, 2.368264730583012234, -3.681130640444375324 ) ) ;
#10571=CARTESIAN_POINT ( 'NONE',  ( 0.3198814748697589860, 4.434118497892181487, -0.3507732604232494666 ) ) ;
#10595=CARTESIAN_POINT ( 'NONE',  ( 1.999999999999989564, -3.464101615137775703, -3.142992957459243453 ) ) ;
#10614=EDGE_CURVE ( 'NONE', #13996, #3137, #12008, .T. ) ;
#10620=CARTESIAN_POINT ( 'NONE',  ( -3.999999999999998224, -1.539600717839010979, -3.300726591567081591 ) ) ;
#10622=VERTEX_POINT ( 'NONE', #1656 ) ;
#10662=CARTESIAN_POINT ( 'NONE',  ( -0.6507732100473468950, 4.243078065514775510, -0.2236248678334808448 ) ) ;
#10666=FILL_AREA_STYLE ('',( #1416 ) ) ;
#10683=ORIENTED_EDGE ( 'NONE', *, *, #13266, .T. ) ;
#10685=AXIS2_PLACEMENT_3D ( 'NONE', #2847, #6394, #1560 ) ;
#10701=( LENGTH_UNIT ( ) NAMED_UNIT ( * ) SI_UNIT ( .MILLI., .METRE. ) );
#10718=ADVANCED_FACE ( 'NONE', ( #5293 ), #1732, .F. ) ;
#10720=PLANE ( 'NONE',  #8074 ) ;
#10725=ORIENTED_EDGE ( 'NONE', *, *, #9588, .F. ) ;
#10730=CARTESIAN_POINT ( 'NONE',  ( 3.999999999999996447, 0.000000000000000000, 0.000000000000000000 ) ) ;
#10731=AXIS2_PLACEMENT_3D ( 'NONE', #13684, #4795, #6836 ) ;
#10733=ORIENTED_EDGE ( 'NONE', *, *, #12412, .F. ) ;
#10734=B_SPLINE_CURVE_WITH_KNOTS ( 'NONE', 3,
 ( #14998, #1327, #2378, #6928, #3455, #1177, #5943, #6993 ),
 .UNSPECIFIED., .F., .F.,
 ( 4, 2, 2, 4 ),
 ( 0.005725059856848643478, 0.006314084072593628347, 0.006903108288338612349, 0.008081156719828581220 ),
 .UNSPECIFIED. ) ;
#10740=CARTESIAN_POINT ( 'NONE',  ( -2.836893136758492862, -3.208949435745870105, -3.505054077164886372 ) ) ;
#10741=EDGE_CURVE ( 'NONE', #9388, #5971, #14642, .T. ) ;
#10745=PLANE ( 'NONE',  #13455 ) ;
#10759=ORIENTED_EDGE ( 'NONE', *, *, #13266, .F. ) ;
#10768=DIRECTION ( 'NONE',  ( 1.000000000000000000, 0.000000000000000000, 0.000000000000000000 ) ) ;
#10786=ADVANCED_FACE ( 'NONE', ( #7793 ), #7617, .T. ) ;
#10801=CARTESIAN_POINT ( 'NONE',  ( 4.198928548860770604, -0.8158838809860120556, -3.526471437616916837 ) ) ;
#10840=CARTESIAN_POINT ( 'NONE',  ( -4.154094228333817362, -2.398367420967598029, -3.721909803043260023 ) ) ;
#10857=CARTESIAN_POINT ( 'NONE',  ( 1.655952806101429031, -3.662737355149044749, -8.872387778173047248E-15 ) ) ;
#10881=UNCERTAINTY_MEASURE_WITH_UNIT (LENGTH_MEASURE( 1.000000000000000082E-05 ), #11982, 'distance_accuracy_value', 'NONE');
#10898=EDGE_LOOP ( 'NONE', ( #10199, #10923, #12916 ) ) ;
#10904=ORIENTED_EDGE ( 'NONE', *, *, #1378, .F. ) ;
#10913=CARTESIAN_POINT ( 'NONE',  ( 3.436319922986348807, -2.634841920958731709, -3.531542292954501505 ) ) ;
#10917=VERTEX_POINT ( 'NONE', #11894 ) ;
#10923=ORIENTED_EDGE ( 'NONE', *, *, #5373, .T. ) ;
#10940=DIRECTION ( 'NONE',  ( 1.000000000000000000, 0.000000000000000000, 0.000000000000000000 ) ) ;
#10959=B_SPLINE_CURVE_WITH_KNOTS ( 'NONE', 3,
 ( #3415, #10394, #6962, #10662, #6814, #64 ),
 .UNSPECIFIED., .F., .F.,
 ( 4, 2, 4 ),
 ( 0.002365888236227972966, 0.003551327329835076308, 0.004736766423442179651 ),
 .UNSPECIFIED. ) ;
#10993=CARTESIAN_POINT ( 'NONE',  ( 4.236525694536555697, -2.416953475386484751, -3.751298745799840795 ) ) ;
#11001=CARTESIAN_POINT ( 'NONE',  ( 2.171643655288381325, -3.365003104552330537, -9.498909814825474384E-15 ) ) ;
#11010=DIRECTION ( 'NONE',  ( 0.000000000000000000, 0.000000000000000000, -1.000000000000000000 ) ) ;
#11023=EDGE_LOOP ( 'NONE', ( #6346, #8054, #7491 ) ) ;
#11031=CARTESIAN_POINT ( 'NONE',  ( 4.197393957002300446, 7.760817478283647932E-14, -3.503767560748928922 ) ) ;
#11063=CARTESIAN_POINT ( 'NONE',  ( 0.000000000000000000, 4.618802153517009401, -3.433295621305381573 ) ) ;
#11066=ORIENTED_EDGE ( 'NONE', *, *, #4552, .F. ) ;
#11068=EDGE_LOOP ( 'NONE', ( #5752, #8223, #9143, #2156, #8312 ) ) ;
#11119=CARTESIAN_POINT ( 'NONE',  ( 3.999999999999998224, 0.8378280264232922381, -3.220590601395640906 ) ) ;
#11120=B_SPLINE_CURVE_WITH_KNOTS ( 'NONE', 3,
 ( #3068, #7828, #5415, #13603, #5263 ),
 .UNSPECIFIED., .F., .F.,
 ( 4, 1, 4 ),
 ( 0.000000000000000000, 0.002309401076758505356, 0.004618802153517009845 ),
 .UNSPECIFIED. ) ;
#11125=EDGE_CURVE ( 'NONE', #7436, #2855, #12415, .T. ) ;
#11172=EDGE_CURVE ( 'NONE', #362, #6726, #11789, .T. ) ;
#11197=CARTESIAN_POINT ( 'NONE',  ( 4.203935335434015208, 1.640780671294171045, -3.598452447879191052 ) ) ;
#11200=CARTESIAN_POINT ( 'NONE',  ( -0.5636800770127728955, -4.293361309317330843, -3.531542292954304774 ) ) ;
#11248=CARTESIAN_POINT ( 'NONE',  ( -2.100000000000000089, 2.571758278209441957E-16, -5.000000000000000888 ) ) ;
#11272=CARTESIAN_POINT ( 'NONE',  ( 3.999999999999998224, -1.700175430507268937, -3.320327275037804782 ) ) ;
#11312=DIRECTION ( 'NONE',  ( -1.000000000000000000, 0.000000000000000000, 0.000000000000000000 ) ) ;
#11335=CARTESIAN_POINT ( 'NONE',  ( 0.000000000000000000, 0.000000000000000000, -4.974599999999998801 ) ) ;
#11343=EDGE_LOOP ( 'NONE', ( #12214, #2697, #4348, #6456, #14268 ) ) ;
#11348=ORIENTED_EDGE ( 'NONE', *, *, #3023, .T. ) ;
#11356=CARTESIAN_POINT ( 'NONE',  ( -1.999999999999997335, 3.464101615137752610, -3.142992957459231906 ) ) ;
#11362=CARTESIAN_POINT ( 'NONE',  ( 0.000000000000000000, 0.000000000000000000, 0.000000000000000000 ) ) ;
#11377=ORIENTED_EDGE ( 'NONE', *, *, #4408, .T. ) ;
#11404=DIRECTION ( 'NONE',  ( 0.000000000000000000, 0.000000000000000000, -1.000000000000000000 ) ) ;
#11420=CARTESIAN_POINT ( 'NONE',  ( 2.500000000000000888, 3.061616997868384127E-16, -4.974599999999998801 ) ) ;
#11442=CONICAL_SURFACE ( 'NONE', #525, 2.059999999999998721, 0.9599310885968738161 ) ;
#11468=CARTESIAN_POINT ( 'NONE',  ( -4.101948962586058123, 2.368261337751160767, -3.681124513963740075 ) ) ;
#11496=CARTESIAN_POINT ( 'NONE',  ( -3.999999999999998224, -2.512220745329311722, -3.469390707569720789 ) ) ;
#11504=CARTESIAN_POINT ( 'NONE',  ( -2.682243648011669368, -3.070208061305315983, -0.04852650426602034966 ) ) ;
#11512=EDGE_CURVE ( 'NONE', #9830, #13811, #4189, .T. ) ;
#11523=EDGE_CURVE ( 'NONE', #12160, #5971, #10959, .T. ) ;
#11548=VERTEX_POINT ( 'NONE', #1147 ) ;
#11558=CARTESIAN_POINT ( 'NONE',  ( 0.02448733951239540421, 4.877042772274725380, -3.751161874094022686 ) ) ;
#11593=CARTESIAN_POINT ( 'NONE',  ( -3.333333333333331705, 2.694301256218250451, -3.300726591567082480 ) ) ;
#11639=ADVANCED_FACE ( 'NONE', ( #1288 ), #6182, .T. ) ;
#11654=AXIS2_PLACEMENT_3D ( 'NONE', #11957, #3756, #8447 ) ;
#11691=ORIENTED_EDGE ( 'NONE', *, *, #12185, .T. ) ;
#11695=EDGE_CURVE ( 'NONE', #12160, #7436, #7852, .T. ) ;
#11703=ORIENTED_EDGE ( 'NONE', *, *, #14090, .T. ) ;
#11705=EDGE_CURVE ( 'NONE', #14140, #5547, #14703, .T. ) ;
#11711=CARTESIAN_POINT ( 'NONE',  ( 2.804994570502170159, 3.229033611042449348, -3.526374918436834260 ) ) ;
#11712=CARTESIAN_POINT ( 'NONE',  ( 2.682243648011666259, 3.070208061305303548, -0.04852650426601186340 ) ) ;
#11743=CIRCLE ( 'NONE', #101, 5.560781378645573980 ) ;
#11750=CARTESIAN_POINT ( 'NONE',  ( 0.5636800770129354321, 4.293361309317172747, -3.531542292955333728 ) ) ;
#11767=ORIENTED_EDGE ( 'NONE', *, *, #12150, .T. ) ;
#11776=ADVANCED_FACE ( 'NONE', ( #8631 ), #6445, .F. ) ;
#11778=CARTESIAN_POINT ( 'NONE',  ( -3.999999999999996447, 2.309401076758498039, -3.433295621305378020 ) ) ;
#11779=VECTOR ( 'NONE', #10323, 1000.000000000000227 ) ;
#11789=LINE ( 'NONE', #8133, #4258 ) ;
#11791=CARTESIAN_POINT ( 'NONE',  ( -2.775557561562891351E-14, -4.618802153517009401, -0.5000000000000004441 ) ) ;
#11793=VERTEX_POINT ( 'NONE', #12514 ) ;
#11801=DIRECTION ( 'NONE',  ( -0.5000000000000019984, -0.8660254037844375974, 0.000000000000000000 ) ) ;
#11822=DIRECTION ( 'NONE',  ( 1.000000000000000000, 0.000000000000000000, 0.000000000000000000 ) ) ;
#11828=ORIENTED_EDGE ( 'NONE', *, *, #9700, .T. ) ;
#11847=VERTEX_POINT ( 'NONE', #8698 ) ;
#11852=CARTESIAN_POINT ( 'NONE',  ( 3.999999999999996447, -1.560351142792951951, -0.2242961665059788889 ) ) ;
#11862=ORIENTED_EDGE ( 'NONE', *, *, #14457, .T. ) ;
#11871=CARTESIAN_POINT ( 'NONE',  ( 4.197393957002299558, -0.4069871074557456780, -3.503767560748925813 ) ) ;
#11880=B_SPLINE_CURVE_WITH_KNOTS ( 'NONE', 3,
 ( #12168, #1763, #631, #5256, #14517, #4115, #6746, #10336 ),
 .UNSPECIFIED., .F., .F.,
 ( 4, 2, 2, 4 ),
 ( 0.005725059856848646080, 0.006314084072593634418, 0.006903108288338622757, 0.008081156719828598567 ),
 .UNSPECIFIED. ) ;
#11894=CARTESIAN_POINT ( 'NONE',  ( 0.000000000000000000, -4.618802153517023612, -3.433295621305388678 ) ) ;
#11898=( NAMED_UNIT ( * ) SI_UNIT ( $, .STERADIAN. ) SOLID_ANGLE_UNIT ( ) );
#11909=CARTESIAN_POINT ( 'NONE',  ( -2.499999999999999556, 3.061616997868382648E-16, 3.469446951953614189E-15 ) ) ;
#11942=CARTESIAN_POINT ( 'NONE',  ( 0.6507732100473456738, -4.243078065514790609, -0.2236248678334918361 ) ) ;
#11943=CARTESIAN_POINT ( 'NONE',  ( -2.000000000000008882, -3.464101615137750390, 0.000000000000000000 ) ) ;
#11954=CARTESIAN_POINT ( 'NONE',  ( 4.197393957002300446, 7.760817478283647932E-14, -3.503767560748928922 ) ) ;
#11957=CARTESIAN_POINT ( 'NONE',  ( 0.000000000000000000, 0.000000000000000000, -4.974599999999998801 ) ) ;
#11974=ORIENTED_EDGE ( 'NONE', *, *, #10614, .F. ) ;
#11982=( LENGTH_UNIT ( ) NAMED_UNIT ( * ) SI_UNIT ( .MILLI., .METRE. ) );
#11996=AXIS2_PLACEMENT_3D ( 'NONE', #8339, #1733, #3941 ) ;
#11999=CARTESIAN_POINT ( 'NONE',  ( 2.807080416178797666, -3.225969019225332524, -3.502507215260528994 ) ) ;
#12008=CIRCLE ( 'NONE', #14909, 2.499999999999999556 ) ;
#12019=ORIENTED_EDGE ( 'NONE', *, *, #4218, .T. ) ;
#12026=CARTESIAN_POINT ( 'NONE',  ( -3.999999999999996447, 2.309401076758498039, -5.000000000000000888 ) ) ;
#12061=ADVANCED_FACE ( 'NONE', ( #2330 ), #2868, .F. ) ;
#12067=CARTESIAN_POINT ( 'NONE',  ( 3.455068668934434317, -2.624017327439083669, -3.316620875263605051 ) ) ;
#12074=ORIENTED_EDGE ( 'NONE', *, *, #7814, .F. ) ;
#12078=ORIENTED_EDGE ( 'NONE', *, *, #11512, .T. ) ;
#12087=B_SPLINE_CURVE_WITH_KNOTS ( 'NONE', 3,
 ( #5319, #4423, #2971, #13449 ),
 .UNSPECIFIED., .F., .F.,
 ( 4, 4 ),
 ( 0.000000000000000000, 0.002452478801916362864 ),
 .UNSPECIFIED. ) ;
#12093=CARTESIAN_POINT ( 'NONE',  ( 3.999999999999996447, 2.309401076758498039, -5.000000000000000888 ) ) ;
#12110=CARTESIAN_POINT ( 'NONE',  ( 0.000000000000000000, -4.618802153517023612, -5.000000000000000888 ) ) ;
#12120=PRODUCT_DEFINITION_FORMATION_WITH_SPECIFIED_SOURCE ( 'ANY', '', #4170, .NOT_KNOWN. ) ;
#12125=AXIS2_PLACEMENT_3D ( 'NONE', #846, #13510, #1970 ) ;
#12137=CARTESIAN_POINT ( 'NONE',  ( 2.712762565639232903, -3.052587955997690283, -3.430618716626819165 ) ) ;
#12144=TOROIDAL_SURFACE ( 'NONE', #5587, 5.384454397937118664, 0.5155456020628804703 ) ;
#12150=EDGE_CURVE ( 'NONE', #10917, #10230, #1650, .T. ) ;
#12160=VERTEX_POINT ( 'NONE', #14393 ) ;
#12168=CARTESIAN_POINT ( 'NONE',  ( 3.999999999999996447, 0.000000000000000000, 0.000000000000000000 ) ) ;
#12185=EDGE_CURVE ( 'NONE', #7535, #7436, #10259, .T. ) ;
#12190=CIRCLE ( 'NONE', #309, 2.499999999999999556 ) ;
#12194=CARTESIAN_POINT ( 'NONE',  ( -2.000000000000008882, -3.464101615137750390, 0.000000000000000000 ) ) ;
#12214=ORIENTED_EDGE ( 'NONE', *, *, #13225, .F. ) ;
#12228=EDGE_CURVE ( 'NONE', #10230, #2995, #9898, .T. ) ;
#12236=VECTOR ( 'NONE', #15007, 1000.000000000000000 ) ;
#12243=ORIENTED_EDGE ( 'NONE', *, *, #9266, .T. ) ;
#12248=ORIENTED_EDGE ( 'NONE', *, *, #11523, .T. ) ;
#12255=DIRECTION ( 'NONE',  ( 0.000000000000000000, 0.000000000000000000, 1.000000000000000000 ) ) ;
#12261=CARTESIAN_POINT ( 'NONE',  ( -4.211140560182194292, 2.431303136016534250, -3.745885042887433958 ) ) ;
#12270=CARTESIAN_POINT ( 'NONE',  ( -3.453038570459854739, -2.625189405340492055, -3.535263753545665022 ) ) ;
#12315=CARTESIAN_POINT ( 'NONE',  ( 0.3461262719736162841, -4.658553426539305597, -3.671615880910381158 ) ) ;
#12337=ORIENTED_EDGE ( 'NONE', *, *, #12830, .F. ) ;
#12348=CARTESIAN_POINT ( 'NONE',  ( 0.000000000000000000, 4.618802153517009401, -3.504269196027870237 ) ) ;
#12362=CARTESIAN_POINT ( 'NONE',  ( 2.855764796983345288, -2.970025579236424296, -0.09382832055446289898 ) ) ;
#12366=ORIENTED_EDGE ( 'NONE', *, *, #1250, .T. ) ;
#12385=FACE_OUTER_BOUND ( 'NONE', #10898, .T. ) ;
#12399=DIRECTION ( 'NONE',  ( -0.000000000000000000, -0.000000000000000000, 1.000000000000000000 ) ) ;
#12407=FACE_OUTER_BOUND ( 'NONE', #7963, .T. ) ;
#12412=EDGE_CURVE ( 'NONE', #9388, #13753, #4185, .T. ) ;
#12415=B_SPLINE_CURVE_WITH_KNOTS ( 'NONE', 3,
 ( #4727, #5705, #11712, #4572, #13990, #13920 ),
 .UNSPECIFIED., .F., .F.,
 ( 4, 2, 4 ),
 ( 0.002365888236227995083, 0.003551327329835084548, 0.004736766423442173579 ),
 .UNSPECIFIED. ) ;
#12419=CARTESIAN_POINT ( 'NONE',  ( 3.999999999999996447, -2.309401076758518911, -5.000000000000000888 ) ) ;
#12435=CARTESIAN_POINT ( 'NONE',  ( 0.000000000000000000, 0.000000000000000000, 0.000000000000000000 ) ) ;
#12504=FACE_OUTER_BOUND ( 'NONE', #7059, .T. ) ;
#12514=CARTESIAN_POINT ( 'NONE',  ( 4.211140560182194292, -2.431303136016555122, -3.745885042887437510 ) ) ;
#12522=CARTESIAN_POINT ( 'NONE',  ( 0.000000000000000000, 0.000000000000000000, -4.000000000000000000 ) ) ;
#12528=DIRECTION ( 'NONE',  ( -1.000000000000000000, 0.000000000000000000, 0.000000000000000000 ) ) ;
#12544=CARTESIAN_POINT ( 'NONE',  ( -4.211140560182194292, -2.431303136016555122, -3.745885042887437510 ) ) ;
#12566=PLANE ( 'NONE',  #779 ) ;
#12596=CARTESIAN_POINT ( 'NONE',  ( 0.000000000000000000, 0.000000000000000000, 0.000000000000000000 ) ) ;
#12600=CARTESIAN_POINT ( 'NONE',  ( -3.455068668934470733, 2.624017327439040592, -3.316620875263627699 ) ) ;
#12636=CARTESIAN_POINT ( 'NONE',  ( -2.171643655288372887, 3.365003104552320323, 1.141800412898796857E-15 ) ) ;
#12648=ORIENTED_EDGE ( 'NONE', *, *, #12412, .T. ) ;
#12651=CARTESIAN_POINT ( 'NONE',  ( 0.000000000000000000, 0.000000000000000000, 0.000000000000000000 ) ) ;
#12687=CARTESIAN_POINT ( 'NONE',  ( -4.211140560182194292, 2.431303136016534250, -3.745885042887433958 ) ) ;
#12716=CARTESIAN_POINT ( 'NONE',  ( -2.855764796983341736, 2.970025579236414082, -0.09382832055445329555 ) ) ;
#12725=FACE_OUTER_BOUND ( 'NONE', #11023, .T. ) ;
#12728=CARTESIAN_POINT ( 'NONE',  ( -3.999999999999997335, -1.560351142792952173, -0.2242961665059789167 ) ) ;
#12749=ORIENTED_EDGE ( 'NONE', *, *, #6528, .T. ) ;
#12754=EDGE_CURVE ( 'NONE', #2530, #4112, #14525, .T. ) ;
#12758=CIRCLE ( 'NONE', #6190, 4.000000000000000000 ) ;
#12765=CARTESIAN_POINT ( 'NONE',  ( -4.197393957002299558, 0.4069871074557440682, -3.503767560748926257 ) ) ;
#12767=SHAPE_REPRESENTATION ( 'hex flange nut gradea_iso_ISO - 4161 - M5 - N', ( #5108 ), #4118 ) ;
#12770=B_SPLINE_CURVE_WITH_KNOTS ( 'NONE', 3,
 ( #3253, #10380, #3475, #13963, #2395, #7874 ),
 .UNSPECIFIED., .F., .F.,
 ( 4, 2, 4 ),
 ( 3.602423855278215334E-18, 0.0002095117440864797216, 0.0004190234881729558111 ),
 .UNSPECIFIED. ) ;
#12772=EDGE_CURVE ( 'NONE', #11548, #2568, #6381, .T. ) ;
#12787=DIRECTION ( 'NONE',  ( 1.000000000000000000, 0.000000000000000000, 0.000000000000000000 ) ) ;
#12808=( NAMED_UNIT ( * ) PLANE_ANGLE_UNIT ( ) SI_UNIT ( $, .RADIAN. ) );
#12830=EDGE_CURVE ( 'NONE', #13811, #6726, #11743, .T. ) ;
#12833=CARTESIAN_POINT ( 'NONE',  ( 3.999999999999996447, -2.309401076758518911, -0.5000000000000004441 ) ) ;
#12881=PRESENTATION_STYLE_ASSIGNMENT (( #2556 ) ) ;
#12909=VERTEX_POINT ( 'NONE', #9043 ) ;
#12916=ORIENTED_EDGE ( 'NONE', *, *, #11125, .F. ) ;
#12917=CARTESIAN_POINT ( 'NONE',  ( 3.861362476283253464, 2.629030857715985992, -3.671615880910370056 ) ) ;
#12921=CARTESIAN_POINT ( 'NONE',  ( -4.000000000000369482, 0.8576368993455062428, -3.433240632782570856 ) ) ;
#12930=CARTESIAN_POINT ( 'NONE',  ( -2.000000000000000000, -3.464101615137773926, -3.142992957459240344 ) ) ;
#12957=DIRECTION ( 'NONE',  ( -0.000000000000000000, -0.000000000000000000, 1.000000000000000000 ) ) ;
#13007=CARTESIAN_POINT ( 'NONE',  ( 1.828356344711641102, 3.563200125723179568, 1.655949411882156916E-16 ) ) ;
#13010=DIRECTION ( 'NONE',  ( 0.8660254037844374864, -0.5000000000000018874, 0.000000000000000000 ) ) ;
#13041=CARTESIAN_POINT ( 'NONE',  ( 2.500000000000000444, 0.000000000000000000, -25.03750572909317285 ) ) ;
#13060=( NAMED_UNIT ( * ) PLANE_ANGLE_UNIT ( ) SI_UNIT ( $, .RADIAN. ) );
#13086=ORIENTED_EDGE ( 'NONE', *, *, #7070, .T. ) ;
#13101=DIRECTION ( 'NONE',  ( 0.000000000000000000, 0.000000000000000000, 1.000000000000000000 ) ) ;
#13107=CARTESIAN_POINT ( 'NONE',  ( 1.287237434361648170, 3.875615274277123934, -3.430618716626443021 ) ) ;
#13115=DIRECTION ( 'NONE',  ( -0.000000000000000000, -0.000000000000000000, 1.000000000000000000 ) ) ;
#13126=CARTESIAN_POINT ( 'NONE',  ( 0.5469614295412751348, -4.303013824935497667, -3.535263753543608001 ) ) ;
#13174=CIRCLE ( 'NONE', #4443, 2.100000000000000089 ) ;
#13202=DIRECTION ( 'NONE',  ( -0.000000000000000000, -0.000000000000000000, 1.000000000000000000 ) ) ;
#13213=AXIS2_PLACEMENT_3D ( 'NONE', #12651, #8227, #2247 ) ;
#13219=ADVANCED_FACE ( 'NONE', ( #4984 ), #6243, .T. ) ;
#13225=EDGE_CURVE ( 'NONE', #9910, #2855, #421, .T. ) ;
#13234=DIRECTION ( 'NONE',  ( -1.000000000000000000, 0.000000000000000000, 0.000000000000000000 ) ) ;
#13238=ORIENTED_EDGE ( 'NONE', *, *, #4589, .F. ) ;
#13266=EDGE_CURVE ( 'NONE', #2530, #9923, #2203, .T. ) ;
#13270=ORIENTED_EDGE ( 'NONE', *, *, #5595, .T. ) ;
#13276=CARTESIAN_POINT ( 'NONE',  ( -3.999999999999996447, -2.309401076758511806, -3.433295621305381573 ) ) ;
#13287=CARTESIAN_POINT ( 'NONE',  ( 4.211140560182194292, 2.431303136016534250, -3.745885042887433958 ) ) ;
#13308=ADVANCED_FACE ( 'NONE', ( #13317 ), #6533, .F. ) ;
#13314=CARTESIAN_POINT ( 'NONE',  ( 4.197478902586991190, -0.8524102783748379597, -3.505063281295504929 ) ) ;
#13317=FACE_OUTER_BOUND ( 'NONE', #10371, .T. ) ;
#13392=CARTESIAN_POINT ( 'NONE',  ( 3.999999999999998224, -0.8578082829537109211, -3.433262215449996102 ) ) ;
#13398=CARTESIAN_POINT ( 'NONE',  ( -2.756197834950063097, -3.027510591568736142, -3.223146290109811130 ) ) ;
#13415=AXIS2_PLACEMENT_3D ( 'NONE', #3698, #12957, #11822 ) ;
#13427=ORIENTED_EDGE ( 'NONE', *, *, #6417, .F. ) ;
#13438=CARTESIAN_POINT ( 'NONE',  ( 5.560781378645573980, 6.809993116116507654E-16, -4.000000000000000000 ) ) ;
#13449=CARTESIAN_POINT ( 'NONE',  ( 4.197393957002300446, 7.760817478283647932E-14, -3.503767560748928922 ) ) ;
#13455=AXIS2_PLACEMENT_3D ( 'NONE', #8536, #14164, #8609 ) ;
#13468=FACE_OUTER_BOUND ( 'NONE', #7323, .T. ) ;
#13471=CARTESIAN_POINT ( 'NONE',  ( 4.204115023516828309, -1.660442669500202140, -3.602151381774573391 ) ) ;
#13493=AXIS2_PLACEMENT_3D ( 'NONE', #9047, #2368, #10414 ) ;
#13510=DIRECTION ( 'NONE',  ( 0.000000000000000000, 0.000000000000000000, -1.000000000000000000 ) ) ;
#13519=DIRECTION ( 'NONE',  ( 0.000000000000000000, 0.000000000000000000, -1.000000000000000000 ) ) ;
#13550=ORIENTED_EDGE ( 'NONE', *, *, #8898, .F. ) ;
#13573=ADVANCED_FACE ( 'NONE', ( #13857 ), #11442, .F. ) ;
#13574=CONICAL_SURFACE ( 'NONE', #2915, 4.000000000000000000, 0.8911886515913786111 ) ;
#13577=EDGE_CURVE ( 'NONE', #5002, #12160, #1023, .T. ) ;
#13593=CARTESIAN_POINT ( 'NONE',  ( -4.197393957002300446, -7.680494662014190109E-14, -3.503767560748928922 ) ) ;
#13600=VECTOR ( 'NONE', #13101, 1000.000000000000000 ) ;
#13602=CARTESIAN_POINT ( 'NONE',  ( -0.3461262719736152849, 4.658553426539284281, -3.671615880910373608 ) ) ;
#13603=CARTESIAN_POINT ( 'NONE',  ( 0.6666666666666655194, 4.233901974057256545, -3.300726591567080259 ) ) ;
#13613=CARTESIAN_POINT ( 'NONE',  ( 3.999999999999998224, 2.512223110932543690, -3.469391141908804599 ) ) ;
#13614=B_SPLINE_CURVE_WITH_KNOTS ( 'NONE', 3,
 ( #4571, #3432, #9338, #1382, #11711, #7972, #12917, #2507 ),
 .UNSPECIFIED., .F., .F.,
 ( 4, 2, 2, 4 ),
 ( 0.000000000000000000, 0.002450665683189819696, 0.003675998524784729327, 0.004901331366379639391 ),
 .UNSPECIFIED. ) ;
#13640=ORIENTED_EDGE ( 'NONE', *, *, #1518, .F. ) ;
#13650=VERTEX_POINT ( 'NONE', #10466 ) ;
#13669=ORIENTED_EDGE ( 'NONE', *, *, #4618, .T. ) ;
#13684=CARTESIAN_POINT ( 'NONE',  ( 0.000000000000000000, 0.000000000000000000, -5.000000000000000888 ) ) ;
#13704=CARTESIAN_POINT ( 'NONE',  ( 0.1756481739660548935, -4.720212674038995360, -3.469390959564072396 ) ) ;
#13729=DIRECTION ( 'NONE',  ( -1.000000000000000000, 0.000000000000000000, 0.000000000000000000 ) ) ;
#13740=ORIENTED_EDGE ( 'NONE', *, *, #5595, .F. ) ;
#13745=CARTESIAN_POINT ( 'NONE',  ( -3.999999999999996447, 2.309401076758498039, -3.433295621305378020 ) ) ;
#13750=DIRECTION ( 'NONE',  ( -0.000000000000000000, -0.000000000000000000, 1.000000000000000000 ) ) ;
#13751=CARTESIAN_POINT ( 'NONE',  ( -1.243802165048849773, 3.900692638707412563, -3.223146290109620615 ) ) ;
#13753=VERTEX_POINT ( 'NONE', #8112 ) ;
#13765=CARTESIAN_POINT ( 'NONE',  ( 0.000000000000000000, 0.000000000000000000, -4.484454397937119197 ) ) ;
#13770=CARTESIAN_POINT ( 'NONE',  ( -3.999999999999998224, -0.8382240730041846666, -3.220610619767136473 ) ) ;
#13774=DIRECTION ( 'NONE',  ( 0.000000000000000000, 0.000000000000000000, -1.000000000000000000 ) ) ;
#13778=ORIENTED_EDGE ( 'NONE', *, *, #5157, .F. ) ;
#13790=ORIENTED_EDGE ( 'NONE', *, *, #11705, .F. ) ;
#13803=ORIENTED_EDGE ( 'NONE', *, *, #3413, .F. ) ;
#13811=VERTEX_POINT ( 'NONE', #1789 ) ;
#13857=FACE_OUTER_BOUND ( 'NONE', #4938, .T. ) ;
#13890=CARTESIAN_POINT ( 'NONE',  ( 3.999999999999995559, 2.309401076758498039, -3.504271511727123922 ) ) ;
#13893=ADVANCED_FACE ( 'NONE', ( #4303 ), #12566, .T. ) ;
#13903=CARTESIAN_POINT ( 'NONE',  ( -4.175648173966052923, 2.207990556236527180, -3.469390959564063071 ) ) ;
#13920=CARTESIAN_POINT ( 'NONE',  ( 3.999999999999996447, 2.309401076758511806, -0.5000000000000004441 ) ) ;
#13923=CARTESIAN_POINT ( 'NONE',  ( -3.999999999999998224, 1.677772373332607092, -3.535253723896766509 ) ) ;
#13940=CARTESIAN_POINT ( 'NONE',  ( -2.000000000000008882, 3.464101615137750390, 0.000000000000000000 ) ) ;
#13949=AXIS2_PLACEMENT_3D ( 'NONE', #746, #4245, #4168 ) ;
#13959=CARTESIAN_POINT ( 'NONE',  ( 4.235886605889390921, 2.417314728048529204, -3.751161874094020465 ) ) ;
#13963=CARTESIAN_POINT ( 'NONE',  ( 4.101954839143200360, -2.368264730583031774, -3.681130640444377988 ) ) ;
#13990=CARTESIAN_POINT ( 'NONE',  ( 3.679171394226030234, 2.494631558665830529, -0.3503314178412461621 ) ) ;
#13991=CARTESIAN_POINT ( 'NONE',  ( 0.000000000000000000, 4.862606272033088928, -3.745885042887437510 ) ) ;
#13996=VERTEX_POINT ( 'NONE', #1863 ) ;
#14000=ADVANCED_FACE ( 'NONE', ( #7622 ), #4908, .T. ) ;
#14033=ORIENTED_EDGE ( 'NONE', *, *, #5983, .T. ) ;
#14051=EDGE_CURVE ( 'NONE', #5002, #13650, #10734, .T. ) ;
#14053=AXIS2_PLACEMENT_3D ( 'NONE', #10487, #10267, #2364 ) ;
#14055=DIRECTION ( 'NONE',  ( 1.000000000000000000, 0.000000000000000000, 0.000000000000000000 ) ) ;
#14064=CARTESIAN_POINT ( 'NONE',  ( 2.000000000000008882, 3.464101615137750390, 0.000000000000000000 ) ) ;
#14084=ORIENTED_EDGE ( 'NONE', *, *, #610, .T. ) ;
#14090=EDGE_CURVE ( 'NONE', #3137, #13996, #12190, .T. ) ;
#14140=VERTEX_POINT ( 'NONE', #474 ) ;
#14145=PLANE ( 'NONE',  #7606 ) ;
#14146=AXIS2_PLACEMENT_3D ( 'NONE', #7330, #3853, #3933 ) ;
#14164=DIRECTION ( 'NONE',  ( -1.000000000000000000, 0.000000000000000000, 0.000000000000000000 ) ) ;
#14174=ORIENTED_EDGE ( 'NONE', *, *, #12754, .F. ) ;
#14209=B_SPLINE_CURVE_WITH_KNOTS ( 'NONE', 3,
 ( #5546, #9867, #14818, #7738, #8952, #14513, #14744, #4111 ),
 .UNSPECIFIED., .F., .F.,
 ( 4, 2, 2, 4 ),
 ( 0.000000000000000000, 0.002450665683189817961, 0.003675998524784728459, 0.004901331366379638524 ),
 .UNSPECIFIED. ) ;
#14226=CIRCLE ( 'NONE', #8400, 2.100000000000000089 ) ;
#14256=ORIENTED_EDGE ( 'NONE', *, *, #9700, .F. ) ;
#14268=ORIENTED_EDGE ( 'NONE', *, *, #11125, .T. ) ;
#14304=AXIS2_PLACEMENT_3D ( 'NONE', #4814, #4593, #9428 ) ;
#14308=EDGE_LOOP ( 'NONE', ( #11377, #9457, #2025, #1804 ) ) ;
#14317=EDGE_CURVE ( 'NONE', #9910, #9388, #11120, .T. ) ;
#14325=ORIENTED_EDGE ( 'NONE', *, *, #14317, .F. ) ;
#14333=PRODUCT_DEFINITION ( 'UNKNOWN', '', #12120, #4065 ) ;
#14355=ORIENTED_EDGE ( 'NONE', *, *, #1378, .T. ) ;
#14364=CARTESIAN_POINT ( 'NONE',  ( -0.6666666666666660745, -4.233901974057272533, -3.300726591567089141 ) ) ;
#14384=UNCERTAINTY_MEASURE_WITH_UNIT (LENGTH_MEASURE( 1.000000000000000082E-05 ), #278, 'distance_accuracy_value', 'NONE');
#14393=CARTESIAN_POINT ( 'NONE',  ( -2.000000000000008882, 3.464101615137750390, 0.000000000000000000 ) ) ;
#14430=FACE_BOUND ( 'NONE', #4551, .T. ) ;
#14450=FACE_OUTER_BOUND ( 'NONE', #6599, .T. ) ;
#14457=EDGE_CURVE ( 'NONE', #14675, #5448, #8065, .T. ) ;
#14493=ORIENTED_EDGE ( 'NONE', *, *, #11172, .F. ) ;
#14495=AXIS2_PLACEMENT_3D ( 'NONE', #12522, #2181, #11312 ) ;
#14513=CARTESIAN_POINT ( 'NONE',  ( -3.510273485745305511, -2.827716139362668635, -3.610536846335888672 ) ) ;
#14517=CARTESIAN_POINT ( 'NONE',  ( 3.999999999999996447, 0.9868501483902626381, -0.09357334158579327932 ) ) ;
#14519=DIRECTION ( 'NONE',  ( -1.000000000000000000, 0.000000000000000000, 0.000000000000000000 ) ) ;
#14522=CYLINDRICAL_SURFACE ( 'NONE', #2666, 2.100000000000000089 ) ;
#14525=LINE ( 'NONE', #3980, #3978 ) ;
#14535=CARTESIAN_POINT ( 'NONE',  ( -4.140404888673274719, -2.228338276487456859, -3.686887068327036943 ) ) ;
#14539=DIRECTION ( 'NONE',  ( -0.5000000000000016653, 0.8660254037844378194, 0.000000000000000000 ) ) ;
#14540=ORIENTED_EDGE ( 'NONE', *, *, #9016, .T. ) ;
#14545=( GEOMETRIC_REPRESENTATION_CONTEXT ( 3 ) GLOBAL_UNCERTAINTY_ASSIGNED_CONTEXT ( ( #14384 ) ) GLOBAL_UNIT_ASSIGNED_CONTEXT ( ( #278, #4915, #11898 ) ) REPRESENTATION_CONTEXT ( 'NONE', 'WORKASPACE' ) );
#14595=ORIENTED_EDGE ( 'NONE', *, *, #8001, .F. ) ;
#14621=CARTESIAN_POINT ( 'NONE',  ( 0.02511973781850741771, -4.877415612947427981, -3.751298745799846568 ) ) ;
#14642=LINE ( 'NONE', #3097, #7120 ) ;
#14652=EDGE_CURVE ( 'NONE', #5322, #2326, #3128, .T. ) ;
#14659=AXIS2_PLACEMENT_3D ( 'NONE', #8744, #12399, #9881 ) ;
#14669=DIRECTION ( 'NONE',  ( -0.000000000000000000, 0.000000000000000000, -1.000000000000000000 ) ) ;
#14675=VERTEX_POINT ( 'NONE', #9409 ) ;
#14696=ORIENTED_EDGE ( 'NONE', *, *, #2945, .F. ) ;
#14701=CARTESIAN_POINT ( 'NONE',  ( 0.000000000000000000, 0.000000000000000000, -25.03750572909317285 ) ) ;
#14703=B_SPLINE_CURVE_WITH_KNOTS ( 'NONE', 3,
 ( #7483, #10840, #372, #4016, #7188, #13276 ),
 .UNSPECIFIED., .F., .F.,
 ( 4, 2, 4 ),
 ( -3.640115492410510249E-06, 0.0002066546034003379048, 0.0004169493222930863250 ),
 .UNSPECIFIED. ) ;
#14721=EDGE_CURVE ( 'NONE', #1683, #4112, #4846, .T. ) ;
#14724=( BOUNDED_SURFACE ( )  B_SPLINE_SURFACE ( 3, 2, ( 
 ( #2295, #87, #9344 ),
 ( #8206, #13923, #8281 ),
 ( #5850, #12921, #2513 ),
 ( #13770, #3517, #7134 ),
 ( #3357, #7976, #6837 ),
 ( #11496, #1096, #10342 ) ),
 .UNSPECIFIED., .F., .F., .F. ) 
 B_SPLINE_SURFACE_WITH_KNOTS ( ( 4, 2, 4 ),
 ( 3, 3 ),
 ( 0.02027752710269158445, 0.02273781595091097299, 0.02519810479913036153 ),
 ( 0.000000000000000000, 1.000000000000000000 ),
 .UNSPECIFIED. ) 
 GEOMETRIC_REPRESENTATION_ITEM ( )  RATIONAL_B_SPLINE_SURFACE ( (
 ( 1.000000000000000000, 0.8047781431712808242, 1.000000000000000000),
 ( 1.000000000000000000, 0.8123773247082141102, 1.000000000000000000),
 ( 1.000000000000000000, 0.8190670192157281093, 1.000000000000000000),
 ( 1.000000000000000000, 0.8192353552909803494, 1.000000000000000000),
 ( 1.000000000000000000, 0.8126132098228610046, 1.000000000000000000),
 ( 1.000000000000000000, 0.8047712465856391439, 1.000000000000000000) ) ) 
 REPRESENTATION_ITEM ( '' )  SURFACE ( )  );
#14731=CARTESIAN_POINT ( 'NONE',  ( 2.345747346278116208, -3.264484291692499429, -0.01223254789874357248 ) ) ;
#14744=CARTESIAN_POINT ( 'NONE',  ( -3.861362476283254352, -2.629030857716006420, -3.671615880910374052 ) ) ;
#14754=CARTESIAN_POINT ( 'NONE',  ( -0.6937372685066672817, 4.453844082567719909, -3.610536846335887340 ) ) ;
#14767=ORIENTED_EDGE ( 'NONE', *, *, #12830, .T. ) ;
#14818=CARTESIAN_POINT ( 'NONE',  ( -1.391697335622808396, -4.043246145443389672, -3.503898532754371242 ) ) ;
#14820=DIRECTION ( 'NONE',  ( -1.000000000000000000, 1.224646799147352714E-16, 0.000000000000000000 ) ) ;
#14857=DIRECTION ( 'NONE',  ( -1.000000000000000000, 0.000000000000000000, 0.000000000000000000 ) ) ;
#14881=VERTEX_POINT ( 'NONE', #13287 ) ;
#14899=CARTESIAN_POINT ( 'NONE',  ( 2.059999999999998721, 0.000000000000000000, -0.3080913168122742518 ) ) ;
#14909=AXIS2_PLACEMENT_3D ( 'NONE', #438, #13202, #6040 ) ;
#14913=FACE_BOUND ( 'NONE', #8657, .T. ) ;
#14943=ADVANCED_FACE ( 'NONE', ( #3266 ), #1325, .F. ) ;
#14957=CARTESIAN_POINT ( 'NONE',  ( 0.000000000000000000, 0.000000000000000000, 0.000000000000000000 ) ) ;
#14988=CARTESIAN_POINT ( 'NONE',  ( 0.000000000000000000, 0.000000000000000000, -4.974599999999998801 ) ) ;
#14998=CARTESIAN_POINT ( 'NONE',  ( -3.999999999999996447, 0.000000000000000000, 0.000000000000000000 ) ) ;
#15007=DIRECTION ( 'NONE',  ( 0.000000000000000000, 0.000000000000000000, 1.000000000000000000 ) ) ;
#15025=CARTESIAN_POINT ( 'NONE',  ( -4.000000000000000888, 2.309401076758495375, -3.504269196027867128 ) ) ;
ENDSEC;
END-ISO-10303-21;
